ISO-10303-21;
HEADER;
FILE_DESCRIPTION (('STEP AP214'),
    '1' );
FILE_NAME ('Part 32,3_Varsayılan.step',
    '2026-10-10T17:45:43',
    ( '' ),
    ( '' ),
    'SwSTEP 2.0',
    'SolidWorks 2024',
    '' );
FILE_SCHEMA (( 'AUTOMOTIVE_DESIGN' ));
ENDSEC;

DATA;
#1=DIRECTION ( 'NONE',  ( -1.000000000000000000, 0.000000000000000000, 0.000000000000000000 ) ) ;
#5=DIRECTION ( 'NONE',  ( -0.000000000000000000, -0.000000000000000000, -1.000000000000000000 ) ) ;
#7=PLANE ( 'NONE',  #4575 ) ;
#9=VECTOR ( 'NONE', #5251, 1000.000000000000000 ) ;
#13=ORIENTED_EDGE ( 'NONE', *, *, #1970, .T. ) ;
#15=AXIS2_PLACEMENT_3D ( 'NONE', #2990, #2506, #3108 ) ;
#16=FACE_OUTER_BOUND ( 'NONE', #1831, .T. ) ;
#19=EDGE_LOOP ( 'NONE', ( #1698, #4393, #5502, #3759 ) ) ;
#20=ORIENTED_EDGE ( 'NONE', *, *, #5697, .F. ) ;
#24=DIRECTION ( 'NONE',  ( -0.000000000000000000, -0.000000000000000000, -1.000000000000000000 ) ) ;
#27=ORIENTED_EDGE ( 'NONE', *, *, #299, .F. ) ;
#32=EDGE_CURVE ( 'NONE', #4635, #4613, #1964, .T. ) ;
#35=CARTESIAN_POINT ( 'NONE',  ( 0.000000000000000000, 25.00000000000000000, -30.00000000000000000 ) ) ;
#36=CIRCLE ( 'NONE', #3210, 17.00000000000000000 ) ;
#41=CARTESIAN_POINT ( 'NONE',  ( -16.23652742703189489, -37.28747423195188304, -115.0000000000000000 ) ) ;
#42=LINE ( 'NONE', #1036, #6075 ) ;
#43=VERTEX_POINT ( 'NONE', #1427 ) ;
#45=ORIENTED_EDGE ( 'NONE', *, *, #5504, .T. ) ;
#49=CARTESIAN_POINT ( 'NONE',  ( 17.00000000000000000, 25.00000000000000000, 0.000000000000000000 ) ) ;
#51=VERTEX_POINT ( 'NONE', #3905 ) ;
#55=CARTESIAN_POINT ( 'NONE',  ( -3.061616997868383043E-15, -25.00000000000000000, -65.00000000000000000 ) ) ;
#60=AXIS2_PLACEMENT_3D ( 'NONE', #399, #4931, #2444 ) ;
#62=LINE ( 'NONE', #3376, #3089 ) ;
#65=DIRECTION ( 'NONE',  ( 1.000000000000000000, 0.000000000000000000, 0.000000000000000000 ) ) ;
#71=ORIENTED_EDGE ( 'NONE', *, *, #5909, .F. ) ;
#72=VECTOR ( 'NONE', #6322, 1000.000000000000000 ) ;
#74=ORIENTED_EDGE ( 'NONE', *, *, #5032, .F. ) ;
#79=CARTESIAN_POINT ( 'NONE',  ( 0.000000000000000000, 0.000000000000000000, -240.0000000000000000 ) ) ;
#80=ORIENTED_EDGE ( 'NONE', *, *, #5837, .T. ) ;
#87=CARTESIAN_POINT ( 'NONE',  ( 0.000000000000000000, 0.000000000000000000, 48.00000000000000000 ) ) ;
#88=ORIENTED_EDGE ( 'NONE', *, *, #6209, .F. ) ;
#94=DIRECTION ( 'NONE',  ( 1.000000000000000000, 0.000000000000000000, 0.000000000000000000 ) ) ;
#97=AXIS2_PLACEMENT_3D ( 'NONE', #4292, #3267, #2839 ) ;
#98=DIRECTION ( 'NONE',  ( -0.000000000000000000, -0.000000000000000000, -1.000000000000000000 ) ) ;
#101=DIRECTION ( 'NONE',  ( 1.000000000000000000, 0.000000000000000000, 0.000000000000000000 ) ) ;
#102=VECTOR ( 'NONE', #3614, 1000.000000000000000 ) ;
#108=EDGE_CURVE ( 'NONE', #4284, #2336, #4223, .T. ) ;
#115=VECTOR ( 'NONE', #1796, 1000.000000000000000 ) ;
#120=CARTESIAN_POINT ( 'NONE',  ( 44.56092774862622719, -29.44644455561813956, -225.0000000000000000 ) ) ;
#124=CARTESIAN_POINT ( 'NONE',  ( 44.56092774862622719, -29.44644455561813956, -240.0000000000000000 ) ) ;
#125=EDGE_CURVE ( 'NONE', #1691, #43, #4114, .T. ) ;
#126=CARTESIAN_POINT ( 'NONE',  ( 0.2052511266213299934, 21.25619793154162807, -45.00000000000000000 ) ) ;
#127=DIRECTION ( 'NONE',  ( -0.000000000000000000, -0.000000000000000000, 1.000000000000000000 ) ) ;
#134=ORIENTED_EDGE ( 'NONE', *, *, #595, .T. ) ;
#146=VERTEX_POINT ( 'NONE', #1090 ) ;
#147=ORIENTED_EDGE ( 'NONE', *, *, #6162, .F. ) ;
#153=DIRECTION ( 'NONE',  ( -0.000000000000000000, -0.000000000000000000, -1.000000000000000000 ) ) ;
#157=VERTEX_POINT ( 'NONE', #5580 ) ;
#158=FACE_OUTER_BOUND ( 'NONE', #3418, .T. ) ;
#161=VERTEX_POINT ( 'NONE', #2156 ) ;
#163=ORIENTED_EDGE ( 'NONE', *, *, #395, .F. ) ;
#165=FACE_OUTER_BOUND ( 'NONE', #2771, .T. ) ;
#168=DIRECTION ( 'NONE',  ( 1.000000000000000000, 0.000000000000000000, 0.000000000000000000 ) ) ;
#171=ORIENTED_EDGE ( 'NONE', *, *, #4573, .F. ) ;
#175=AXIS2_PLACEMENT_3D ( 'NONE', #388, #2953, #1897 ) ;
#178=EDGE_LOOP ( 'NONE', ( #2214, #4560 ) ) ;
#179=EDGE_LOOP ( 'NONE', ( #3932, #3010 ) ) ;
#180=CARTESIAN_POINT ( 'NONE',  ( -17.00000000000000000, 2.081899558550500280E-15, -273.0000000000000000 ) ) ;
#181=DIRECTION ( 'NONE',  ( -0.000000000000000000, -0.000000000000000000, -1.000000000000000000 ) ) ;
#183=DIRECTION ( 'NONE',  ( -0.000000000000000000, -0.000000000000000000, 1.000000000000000000 ) ) ;
#186=ORIENTED_EDGE ( 'NONE', *, *, #4679, .F. ) ;
#189=EDGE_CURVE ( 'NONE', #3628, #146, #1775, .T. ) ;
#195=CIRCLE ( 'NONE', #5537, 17.00000000000000000 ) ;
#199=CARTESIAN_POINT ( 'NONE',  ( -22.21770253897231839, -3.871672004621880436, 0.000000000000000000 ) ) ;
#201=DIRECTION ( 'NONE',  ( 1.000000000000000000, 0.000000000000000000, 0.000000000000000000 ) ) ;
#204=LINE ( 'NONE', #2155, #1735 ) ;
#205=CIRCLE ( 'NONE', #3492, 45.99999999999997868 ) ;
#206=DIRECTION ( 'NONE',  ( -0.000000000000000000, -0.000000000000000000, 1.000000000000000000 ) ) ;
#214=VERTEX_POINT ( 'NONE', #1745 ) ;
#215=AXIS2_PLACEMENT_3D ( 'NONE', #4568, #5162, #623 ) ;
#217=CARTESIAN_POINT ( 'NONE',  ( 44.00000000000008527, 13.41640786499836224, -160.0000000000000284 ) ) ;
#220=CARTESIAN_POINT ( 'NONE',  ( 44.43364355155687662, -29.42304313293534790, -45.00000000000000000 ) ) ;
#224=ORIENTED_EDGE ( 'NONE', *, *, #2464, .T. ) ;
#226=ORIENTED_EDGE ( 'NONE', *, *, #6094, .T. ) ;
#229=CARTESIAN_POINT ( 'NONE',  ( -0.2052511266214760433, -21.25619793154163517, -65.00000000000000000 ) ) ;
#232=CARTESIAN_POINT ( 'NONE',  ( 44.00000000000000000, -13.41640786499873705, -45.00000000000000000 ) ) ;
#236=DIRECTION ( 'NONE',  ( -0.000000000000000000, 0.000000000000000000, -1.000000000000000000 ) ) ;
#239=ORIENTED_EDGE ( 'NONE', *, *, #5930, .F. ) ;
#242=CARTESIAN_POINT ( 'NONE',  ( -0.2052511266214760433, -21.25619793154163517, -160.0000000000000284 ) ) ;
#244=DIRECTION ( 'NONE',  ( 0.000000000000000000, 0.000000000000000000, -1.000000000000000000 ) ) ;
#245=FACE_OUTER_BOUND ( 'NONE', #526, .T. ) ;
#250=ORIENTED_EDGE ( 'NONE', *, *, #4382, .T. ) ;
#253=ORIENTED_EDGE ( 'NONE', *, *, #3958, .T. ) ;
#254=DIRECTION ( 'NONE',  ( 1.000000000000000000, 0.000000000000000000, 0.000000000000000000 ) ) ;
#260=EDGE_LOOP ( 'NONE', ( #5116, #2752, #3718, #1984 ) ) ;
#262=CARTESIAN_POINT ( 'NONE',  ( -44.00000000000000000, -13.41640786499873350, -180.0000000000000000 ) ) ;
#268=ORIENTED_EDGE ( 'NONE', *, *, #3411, .F. ) ;
#269=ORIENTED_EDGE ( 'NONE', *, *, #3444, .T. ) ;
#271=ADVANCED_FACE ( 'NONE', ( #158 ), #1142, .T. ) ;
#275=DIRECTION ( 'NONE',  ( -1.000000000000000000, 0.000000000000000000, 0.000000000000000000 ) ) ;
#278=CARTESIAN_POINT ( 'NONE',  ( 0.000000000000000000, 0.000000000000000000, -115.0000000000000000 ) ) ;
#285=ORIENTED_EDGE ( 'NONE', *, *, #6012, .F. ) ;
#286=CYLINDRICAL_SURFACE ( 'NONE', #1017, 45.99999999999997868 ) ;
#289=DIRECTION ( 'NONE',  ( -1.000000000000000000, 0.000000000000000000, 0.000000000000000000 ) ) ;
#290=CARTESIAN_POINT ( 'NONE',  ( 0.000000000000000000, 0.000000000000000000, 0.000000000000000000 ) ) ;
#292=CARTESIAN_POINT ( 'NONE',  ( 44.00000000000000000, -13.41640786499873705, -45.00000000000000000 ) ) ;
#293=AXIS2_PLACEMENT_3D ( 'NONE', #3650, #5626, #3015 ) ;
#299=EDGE_CURVE ( 'NONE', #686, #51, #842, .T. ) ;
#301=CARTESIAN_POINT ( 'NONE',  ( 44.43364355155687662, -29.42304313293534790, -180.0000000000000000 ) ) ;
#302=AXIS2_PLACEMENT_3D ( 'NONE', #35, #5903, #5416 ) ;
#305=EDGE_CURVE ( 'NONE', #5346, #4831, #1115, .T. ) ;
#306=VERTEX_POINT ( 'NONE', #1172 ) ;
#312=DIRECTION ( 'NONE',  ( -0.000000000000000000, 0.000000000000000000, -1.000000000000000000 ) ) ;
#313=EDGE_CURVE ( 'NONE', #2336, #4284, #725, .T. ) ;
#320=DIRECTION ( 'NONE',  ( -0.000000000000000000, -0.000000000000000000, 1.000000000000000000 ) ) ;
#325=CARTESIAN_POINT ( 'NONE',  ( -19.00000000000000000, 2.326828918379970970E-15, -248.0000000000000000 ) ) ;
#327=EDGE_CURVE ( 'NONE', #4956, #1995, #4828, .T. ) ;
#329=AXIS2_PLACEMENT_3D ( 'NONE', #4721, #320, #1790 ) ;
#330=SHAPE_REPRESENTATION_RELATIONSHIP ( 'NONE' , 'NONE' ,  #5199, #2789 ) ;
#342=ORIENTED_EDGE ( 'NONE', *, *, #3066, .F. ) ;
#344=DIRECTION ( 'NONE',  ( 1.000000000000000000, 0.000000000000000000, 0.000000000000000000 ) ) ;
#346=FACE_OUTER_BOUND ( 'NONE', #5806, .T. ) ;
#347=EDGE_LOOP ( 'NONE', ( #3523, #3999, #1718, #5180 ) ) ;
#350=AXIS2_PLACEMENT_3D ( 'NONE', #4646, #3102, #2588 ) ;
#363=EDGE_CURVE ( 'NONE', #4783, #2333, #5736, .T. ) ;
#367=DIRECTION ( 'NONE',  ( -0.000000000000000000, -0.000000000000000000, -1.000000000000000000 ) ) ;
#368=DIRECTION ( 'NONE',  ( 0.000000000000000000, 0.000000000000000000, -1.000000000000000000 ) ) ;
#370=ORIENTED_EDGE ( 'NONE', *, *, #6217, .T. ) ;
#382=CIRCLE ( 'NONE', #5939, 90.00000000000319744 ) ;
#383=AXIS2_PLACEMENT_3D ( 'NONE', #932, #2408, #6282 ) ;
#387=ADVANCED_FACE ( 'NONE', ( #4260 ), #5210, .T. ) ;
#388=CARTESIAN_POINT ( 'NONE',  ( 0.000000000000000000, 25.00000000000000000, -30.00000000000000000 ) ) ;
#390=EDGE_CURVE ( 'NONE', #5661, #673, #5569, .T. ) ;
#391=DIRECTION ( 'NONE',  ( -1.000000000000000000, 0.000000000000000000, 0.000000000000000000 ) ) ;
#395=EDGE_CURVE ( 'NONE', #5724, #1881, #5157, .T. ) ;
#396=CARTESIAN_POINT ( 'NONE',  ( 0.000000000000000000, 0.000000000000000000, -65.00000000000000000 ) ) ;
#399=CARTESIAN_POINT ( 'NONE',  ( 0.000000000000000000, 0.000000000000000000, 48.00000000000000000 ) ) ;
#401=ADVANCED_FACE ( 'NONE', ( #6178 ), #5246, .T. ) ;
#406=CIRCLE ( 'NONE', #2964, 17.00000000000000000 ) ;
#410=CARTESIAN_POINT ( 'NONE',  ( 16.23652742703164620, 37.28747423195200383, 0.000000000000000000 ) ) ;
#416=AXIS2_PLACEMENT_3D ( 'NONE', #2228, #2708, #5621 ) ;
#422=AXIS2_PLACEMENT_3D ( 'NONE', #4770, #2723, #5320 ) ;
#423=CARTESIAN_POINT ( 'NONE',  ( 17.00000000000000000, 2.081899558550500280E-15, -180.0000000000000000 ) ) ;
#425=DIRECTION ( 'NONE',  ( 1.000000000000000000, 0.000000000000000000, 0.000000000000000000 ) ) ;
#427=VERTEX_POINT ( 'NONE', #3878 ) ;
#436=CIRCLE ( 'NONE', #2788, 46.00000000000000000 ) ;
#439=CARTESIAN_POINT ( 'NONE',  ( 13.14183123006952947, -39.58265509608667543, -49.99999999999999289 ) ) ;
#441=EDGE_LOOP ( 'NONE', ( #370, #4762, #5262, #4318 ) ) ;
#447=ORIENTED_EDGE ( 'NONE', *, *, #662, .T. ) ;
#453=VERTEX_POINT ( 'NONE', #2946 ) ;
#457=FACE_BOUND ( 'NONE', #4717, .T. ) ;
#458=LINE ( 'NONE', #232, #5970 ) ;
#460=CARTESIAN_POINT ( 'NONE',  ( 16.99999999999999645, -24.99999999999999645, -160.0000000000000000 ) ) ;
#467=CARTESIAN_POINT ( 'NONE',  ( 19.00000000000000000, 0.000000000000000000, -240.0000000000000000 ) ) ;
#469=ORIENTED_EDGE ( 'NONE', *, *, #2472, .F. ) ;
#474=ORIENTED_EDGE ( 'NONE', *, *, #5909, .T. ) ;
#476=AXIS2_PLACEMENT_3D ( 'NONE', #5538, #5967, #2537 ) ;
#483=EDGE_CURVE ( 'NONE', #43, #3426, #961, .T. ) ;
#485=AXIS2_PLACEMENT_3D ( 'NONE', #747, #4694, #6145 ) ;
#489=CARTESIAN_POINT ( 'NONE',  ( 17.00000000000000000, 2.081899558550500280E-15, -175.0000000000000000 ) ) ;
#505=DIRECTION ( 'NONE',  ( 0.000000000000000000, 0.000000000000000000, -1.000000000000000000 ) ) ;
#507=CYLINDRICAL_SURFACE ( 'NONE', #605, 22.67164836619066648 ) ;
#510=AXIS2_PLACEMENT_3D ( 'NONE', #2170, #6108, #5525 ) ;
#515=DIRECTION ( 'NONE',  ( -0.000000000000000000, -0.000000000000000000, 1.000000000000000000 ) ) ;
#517=EDGE_CURVE ( 'NONE', #51, #146, #2675, .T. ) ;
#518=PLANE ( 'NONE',  #2853 ) ;
#526=EDGE_LOOP ( 'NONE', ( #3915, #2358, #2129, #2824 ) ) ;
#528=AXIS2_PLACEMENT_3D ( 'NONE', #2486, #3029, #1942 ) ;
#530=DIRECTION ( 'NONE',  ( -0.000000000000000000, -0.000000000000000000, 1.000000000000000000 ) ) ;
#535=( NAMED_UNIT ( * ) PLANE_ANGLE_UNIT ( ) SI_UNIT ( $, .RADIAN. ) );
#537=CARTESIAN_POINT ( 'NONE',  ( 0.000000000000000000, 25.00000000000000000, -225.0000000000000000 ) ) ;
#539=CYLINDRICAL_SURFACE ( 'NONE', #6196, 89.87058297576894006 ) ;
#542=VERTEX_POINT ( 'NONE', #5283 ) ;
#543=EDGE_LOOP ( 'NONE', ( #3781, #3174, #5864, #4593 ) ) ;
#546=DIRECTION ( 'NONE',  ( -0.000000000000000000, 0.000000000000000000, -1.000000000000000000 ) ) ;
#550=ORIENTED_EDGE ( 'NONE', *, *, #4554, .F. ) ;
#553=DIRECTION ( 'NONE',  ( -0.000000000000000000, -0.000000000000000000, -1.000000000000000000 ) ) ;
#561=FACE_OUTER_BOUND ( 'NONE', #3544, .T. ) ;
#566=DIRECTION ( 'NONE',  ( 1.000000000000000000, 0.000000000000000000, 0.000000000000000000 ) ) ;
#567=ORIENTED_EDGE ( 'NONE', *, *, #125, .T. ) ;
#569=CIRCLE ( 'NONE', #3996, 17.00000000000000000 ) ;
#570=ORIENTED_EDGE ( 'NONE', *, *, #988, .F. ) ;
#571=CARTESIAN_POINT ( 'NONE',  ( 44.64065620456912598, 28.99954194078667413, -160.0000000000000284 ) ) ;
#572=DIRECTION ( 'NONE',  ( -0.000000000000000000, -0.000000000000000000, 1.000000000000000000 ) ) ;
#573=CYLINDRICAL_SURFACE ( 'NONE', #5444, 89.87058297576894006 ) ;
#577=DIRECTION ( 'NONE',  ( -0.000000000000000000, -0.000000000000000000, 1.000000000000000000 ) ) ;
#585=AXIS2_PLACEMENT_3D ( 'NONE', #4125, #6104, #5138 ) ;
#587=AXIS2_PLACEMENT_3D ( 'NONE', #5409, #4922, #1833 ) ;
#588=EDGE_CURVE ( 'NONE', #3260, #713, #5667, .T. ) ;
#589=DIRECTION ( 'NONE',  ( -0.000000000000000000, -0.000000000000000000, 1.000000000000000000 ) ) ;
#591=AXIS2_PLACEMENT_3D ( 'NONE', #5540, #4567, #168 ) ;
#595=EDGE_CURVE ( 'NONE', #5536, #1071, #2161, .T. ) ;
#600=ADVANCED_FACE ( 'NONE', ( #1021 ), #2589, .T. ) ;
#601=ORIENTED_EDGE ( 'NONE', *, *, #363, .T. ) ;
#602=VERTEX_POINT ( 'NONE', #1583 ) ;
#603=ADVANCED_FACE ( 'NONE', ( #4032 ), #1136, .T. ) ;
#604=EDGE_LOOP ( 'NONE', ( #4129, #2093, #1661, #1916 ) ) ;
#605=AXIS2_PLACEMENT_3D ( 'NONE', #4876, #5431, #2069 ) ;
#606=CARTESIAN_POINT ( 'NONE',  ( -19.00000000000000000, 0.000000000000000000, 23.00000000000000000 ) ) ;
#608=DIRECTION ( 'NONE',  ( 1.000000000000000000, 0.000000000000000000, 0.000000000000000000 ) ) ;
#613=FACE_OUTER_BOUND ( 'NONE', #4079, .T. ) ;
#614=ORIENTED_EDGE ( 'NONE', *, *, #5533, .T. ) ;
#619=VECTOR ( 'NONE', #1169, 1000.000000000000000 ) ;
#620=FACE_OUTER_BOUND ( 'NONE', #1678, .T. ) ;
#623=DIRECTION ( 'NONE',  ( 1.000000000000000000, 0.000000000000000000, 0.000000000000000000 ) ) ;
#624=VERTEX_POINT ( 'NONE', #2522 ) ;
#628=AXIS2_PLACEMENT_3D ( 'NONE', #2918, #553, #1542 ) ;
#631=CARTESIAN_POINT ( 'NONE',  ( -44.43364355155666345, 29.42304313293564988, -115.0000000000000000 ) ) ;
#639=FACE_OUTER_BOUND ( 'NONE', #3277, .T. ) ;
#642=DIRECTION ( 'NONE',  ( 1.000000000000000000, 0.000000000000000000, 0.000000000000000000 ) ) ;
#652=EDGE_LOOP ( 'NONE', ( #1890, #1670, #5992, #4403 ) ) ;
#658=DIRECTION ( 'NONE',  ( 1.000000000000000000, 0.000000000000000000, 0.000000000000000000 ) ) ;
#662=EDGE_CURVE ( 'NONE', #2268, #1338, #5885, .T. ) ;
#670=ADVANCED_FACE ( 'NONE', ( #639 ), #3012, .T. ) ;
#673=VERTEX_POINT ( 'NONE', #2046 ) ;
#681=CARTESIAN_POINT ( 'NONE',  ( -44.43364355155666345, 29.42304313293564988, -110.0000000000000000 ) ) ;
#683=CARTESIAN_POINT ( 'NONE',  ( 0.000000000000000000, 0.000000000000000000, 15.00000000000000000 ) ) ;
#685=DIRECTION ( 'NONE',  ( -0.000000000000000000, -0.000000000000000000, -1.000000000000000000 ) ) ;
#686=VERTEX_POINT ( 'NONE', #3528 ) ;
#687=DIRECTION ( 'NONE',  ( -0.000000000000000000, -0.000000000000000000, 1.000000000000000000 ) ) ;
#688=CARTESIAN_POINT ( 'NONE',  ( -3.061616997868383043E-15, -25.00000000000000000, -160.0000000000000000 ) ) ;
#691=AXIS2_PLACEMENT_3D ( 'NONE', #5866, #899, #4889 ) ;
#694=CYLINDRICAL_SURFACE ( 'NONE', #2563, 17.00000000000000000 ) ;
#697=DIRECTION ( 'NONE',  ( -0.000000000000000000, -0.000000000000000000, 1.000000000000000000 ) ) ;
#702=DIRECTION ( 'NONE',  ( 0.000000000000000000, 0.000000000000000000, 1.000000000000000000 ) ) ;
#704=CIRCLE ( 'NONE', #1097, 22.67164836619066648 ) ;
#708=VECTOR ( 'NONE', #6348, 1000.000000000000000 ) ;
#711=ORIENTED_EDGE ( 'NONE', *, *, #938, .T. ) ;
#713=VERTEX_POINT ( 'NONE', #1711 ) ;
#715=CARTESIAN_POINT ( 'NONE',  ( -2.385244779468109755E-15, -1.040834085586084257E-14, -95.00000000000000000 ) ) ;
#716=CYLINDRICAL_SURFACE ( 'NONE', #4439, 22.67164836619067714 ) ;
#725=CIRCLE ( 'NONE', #5871, 17.00000000000000000 ) ;
#727=AXIS2_PLACEMENT_3D ( 'NONE', #2541, #1976, #3964 ) ;
#729=ORIENTED_EDGE ( 'NONE', *, *, #3131, .T. ) ;
#730=EDGE_LOOP ( 'NONE', ( #3326, #5717, #4359, #2877 ) ) ;
#731=AXIS2_PLACEMENT_3D ( 'NONE', #3118, #4634, #1669 ) ;
#734=DIRECTION ( 'NONE',  ( -0.000000000000000000, -0.000000000000000000, 1.000000000000000000 ) ) ;
#735=AXIS2_PLACEMENT_3D ( 'NONE', #936, #3474, #1933 ) ;
#738=VERTEX_POINT ( 'NONE', #793 ) ;
#743=CARTESIAN_POINT ( 'NONE',  ( -44.00000000000000000, -13.41640786499873350, -45.00000000000000000 ) ) ;
#744=ORIENTED_EDGE ( 'NONE', *, *, #3889, .T. ) ;
#746=ADVANCED_FACE ( 'NONE', ( #1268 ), #4618, .T. ) ;
#747=CARTESIAN_POINT ( 'NONE',  ( 0.000000000000000000, 25.00000000000000000, -195.0000000000000000 ) ) ;
#750=DIRECTION ( 'NONE',  ( 1.000000000000000000, 0.000000000000000000, 0.000000000000000000 ) ) ;
#752=EDGE_CURVE ( 'NONE', #673, #542, #2133, .T. ) ;
#755=ORIENTED_EDGE ( 'NONE', *, *, #988, .T. ) ;
#760=VERTEX_POINT ( 'NONE', #5655 ) ;
#764=LINE ( 'NONE', #3587, #1849 ) ;
#768=VERTEX_POINT ( 'NONE', #2167 ) ;
#769=DIRECTION ( 'NONE',  ( -1.000000000000000000, 0.000000000000000000, 0.000000000000000000 ) ) ;
#773=ADVANCED_FACE ( 'NONE', ( #1755 ), #1233, .T. ) ;
#777=DIRECTION ( 'NONE',  ( -1.000000000000000000, 0.000000000000000000, 0.000000000000000000 ) ) ;
#778=CARTESIAN_POINT ( 'NONE',  ( 2.380270672502711906E-15, -5.204170427930421283E-15, -195.0000000000000000 ) ) ;
#779=DIRECTION ( 'NONE',  ( 0.000000000000000000, 0.000000000000000000, -1.000000000000000000 ) ) ;
#785=ADVANCED_FACE ( 'NONE', ( #6077, #2707 ), #2227, .T. ) ;
#788=DIRECTION ( 'NONE',  ( -1.000000000000000000, 0.000000000000000000, 0.000000000000000000 ) ) ;
#789=ORIENTED_EDGE ( 'NONE', *, *, #2310, .T. ) ;
#793=CARTESIAN_POINT ( 'NONE',  ( 17.00000000000000000, 2.081899558550500280E-15, 23.00000000000000000 ) ) ;
#795=CYLINDRICAL_SURFACE ( 'NONE', #825, 90.00000000000000000 ) ;
#798=ORIENTED_EDGE ( 'NONE', *, *, #363, .F. ) ;
#799=CARTESIAN_POINT ( 'NONE',  ( -44.00000000000000000, -13.41640786499873350, -30.00000000000000000 ) ) ;
#801=EDGE_CURVE ( 'NONE', #713, #5661, #382, .T. ) ;
#803=DIRECTION ( 'NONE',  ( -1.000000000000000000, 0.000000000000000000, 0.000000000000000000 ) ) ;
#805=ORIENTED_EDGE ( 'NONE', *, *, #6094, .F. ) ;
#810=CARTESIAN_POINT ( 'NONE',  ( 0.000000000000000000, 0.000000000000000000, -49.99999999999999289 ) ) ;
#811=CIRCLE ( 'NONE', #4502, 89.87058297576894006 ) ;
#813=ORIENTED_EDGE ( 'NONE', *, *, #1612, .T. ) ;
#822=AXIS2_PLACEMENT_3D ( 'NONE', #4680, #2681, #1234 ) ;
#825=AXIS2_PLACEMENT_3D ( 'NONE', #2264, #4127, #6205 ) ;
#830=ORIENTED_EDGE ( 'NONE', *, *, #483, .T. ) ;
#839=CARTESIAN_POINT ( 'NONE',  ( 0.000000000000000000, 0.000000000000000000, -240.0000000000000000 ) ) ;
#840=ORIENTED_EDGE ( 'NONE', *, *, #305, .F. ) ;
#841=DIRECTION ( 'NONE',  ( -0.000000000000000000, -0.000000000000000000, 1.000000000000000000 ) ) ;
#842=CIRCLE ( 'NONE', #1437, 90.00000000000000000 ) ;
#858=DIRECTION ( 'NONE',  ( 1.000000000000000000, 0.000000000000000000, 0.000000000000000000 ) ) ;
#875=EDGE_CURVE ( 'NONE', #306, #2898, #5816, .T. ) ;
#879=DIRECTION ( 'NONE',  ( 1.000000000000000000, 0.000000000000000000, 0.000000000000000000 ) ) ;
#882=CARTESIAN_POINT ( 'NONE',  ( -13.14183123006980480, 39.58265509608657595, -180.0000000000000000 ) ) ;
#885=ORIENTED_EDGE ( 'NONE', *, *, #305, .T. ) ;
#887=DIRECTION ( 'NONE',  ( -0.000000000000000000, -0.000000000000000000, 1.000000000000000000 ) ) ;
#889=PLANE ( 'NONE',  #1635 ) ;
#899=DIRECTION ( 'NONE',  ( 0.000000000000000000, 0.000000000000000000, -1.000000000000000000 ) ) ;
#904=ORIENTED_EDGE ( 'NONE', *, *, #4382, .F. ) ;
#907=CARTESIAN_POINT ( 'NONE',  ( -3.061616997868383043E-15, -25.00000000000000000, -130.0000000000000000 ) ) ;
#909=DIRECTION ( 'NONE',  ( 0.000000000000000000, 0.000000000000000000, 1.000000000000000000 ) ) ;
#911=ORIENTED_EDGE ( 'NONE', *, *, #3393, .F. ) ;
#913=AXIS2_PLACEMENT_3D ( 'NONE', #4319, #5208, #2232 ) ;
#917=CARTESIAN_POINT ( 'NONE',  ( -44.43364355155666345, 29.42304313293565343, -49.99999999999999289 ) ) ;
#918=CARTESIAN_POINT ( 'NONE',  ( 0.000000000000000000, 0.000000000000000000, -115.0000000000000000 ) ) ;
#920=CARTESIAN_POINT ( 'NONE',  ( 0.000000000000000000, 0.000000000000000000, -175.0000000000000284 ) ) ;
#922=ORIENTED_EDGE ( 'NONE', *, *, #1260, .F. ) ;
#926=CARTESIAN_POINT ( 'NONE',  ( -0.2052511266214760433, -21.25619793154163517, -160.0000000000000284 ) ) ;
#932=CARTESIAN_POINT ( 'NONE',  ( 0.000000000000000000, 0.000000000000000000, -180.0000000000000000 ) ) ;
#936=CARTESIAN_POINT ( 'NONE',  ( 44.43364355155687662, -29.42304313293534790, -195.0000000000000000 ) ) ;
#937=ORIENTED_EDGE ( 'NONE', *, *, #5904, .T. ) ;
#938=EDGE_CURVE ( 'NONE', #5509, #2206, #3462, .T. ) ;
#942=VECTOR ( 'NONE', #515, 1000.000000000000000 ) ;
#951=DIRECTION ( 'NONE',  ( -1.000000000000000000, 0.000000000000000000, 0.000000000000000000 ) ) ;
#954=AXIS2_PLACEMENT_3D ( 'NONE', #5775, #5188, #1351 ) ;
#955=PLANE ( 'NONE',  #2021 ) ;
#957=DIRECTION ( 'NONE',  ( 0.000000000000000000, -0.000000000000000000, 1.000000000000000000 ) ) ;
#960=ORIENTED_EDGE ( 'NONE', *, *, #5044, .T. ) ;
#961=LINE ( 'NONE', #4434, #942 ) ;
#968=EDGE_CURVE ( 'NONE', #1691, #1557, #2295, .T. ) ;
#970=FACE_OUTER_BOUND ( 'NONE', #3101, .T. ) ;
#971=ORIENTED_EDGE ( 'NONE', *, *, #2591, .F. ) ;
#977=DIRECTION ( 'NONE',  ( 0.000000000000000000, -0.000000000000000000, 1.000000000000000000 ) ) ;
#978=ORIENTED_EDGE ( 'NONE', *, *, #3238, .T. ) ;
#981=VERTEX_POINT ( 'NONE', #6328 ) ;
#982=DIRECTION ( 'NONE',  ( 1.000000000000000000, 0.000000000000000000, 0.000000000000000000 ) ) ;
#983=ADVANCED_FACE ( 'NONE', ( #5851, #5886 ), #955, .T. ) ;
#986=CARTESIAN_POINT ( 'NONE',  ( 44.64065620456912598, 28.99954194078667413, -115.0000000000000000 ) ) ;
#988=EDGE_CURVE ( 'NONE', #2898, #2909, #4798, .T. ) ;
#992=CIRCLE ( 'NONE', #5075, 90.00000000000321165 ) ;
#993=DIRECTION ( 'NONE',  ( -0.000000000000000000, -0.000000000000000000, -1.000000000000000000 ) ) ;
#994=VECTOR ( 'NONE', #1447, 1000.000000000000000 ) ;
#998=CARTESIAN_POINT ( 'NONE',  ( -44.64065620456596406, -28.99954194078535963, 15.00000000000000000 ) ) ;
#1000=FACE_OUTER_BOUND ( 'NONE', #6254, .T. ) ;
#1001=LINE ( 'NONE', #489, #2259 ) ;
#1003=DIRECTION ( 'NONE',  ( -0.000000000000000000, -0.000000000000000000, -1.000000000000000000 ) ) ;
#1004=CARTESIAN_POINT ( 'NONE',  ( 17.00000000000000000, 0.000000000000000000, -115.0000000000000000 ) ) ;
#1006=CARTESIAN_POINT ( 'NONE',  ( -17.00000000000000000, 2.081899558550500280E-15, -115.0000000000000000 ) ) ;
#1012=AXIS2_PLACEMENT_3D ( 'NONE', #3258, #368, #2323 ) ;
#1014=CARTESIAN_POINT ( 'NONE',  ( 22.21770253897382474, 3.871672004622519037, -95.00000000000000000 ) ) ;
#1016=ORIENTED_EDGE ( 'NONE', *, *, #2472, .T. ) ;
#1017=AXIS2_PLACEMENT_3D ( 'NONE', #2237, #5695, #1277 ) ;
#1018=ORIENTED_EDGE ( 'NONE', *, *, #4355, .F. ) ;
#1019=VERTEX_POINT ( 'NONE', #1466 ) ;
#1021=FACE_OUTER_BOUND ( 'NONE', #3299, .T. ) ;
#1024=ORIENTED_EDGE ( 'NONE', *, *, #395, .T. ) ;
#1031=DIRECTION ( 'NONE',  ( -1.000000000000000000, 0.000000000000000000, 0.000000000000000000 ) ) ;
#1032=DIRECTION ( 'NONE',  ( -1.000000000000000000, 0.000000000000000000, 0.000000000000000000 ) ) ;
#1036=CARTESIAN_POINT ( 'NONE',  ( -43.99999999999987921, 13.41640786499904969, -110.0000000000000000 ) ) ;
#1037=ORIENTED_EDGE ( 'NONE', *, *, #5028, .T. ) ;
#1038=AXIS2_PLACEMENT_3D ( 'NONE', #6110, #1720, #769 ) ;
#1044=VERTEX_POINT ( 'NONE', #3421 ) ;
#1049=CARTESIAN_POINT ( 'NONE',  ( 0.2052511266213299934, 21.25619793154162807, -180.0000000000000000 ) ) ;
#1056=EDGE_LOOP ( 'NONE', ( #5923, #2799, #5555, #2712 ) ) ;
#1058=EDGE_CURVE ( 'NONE', #602, #51, #1886, .T. ) ;
#1062=CARTESIAN_POINT ( 'NONE',  ( -44.43364355155666345, 29.42304313293564988, -115.0000000000000000 ) ) ;
#1065=( NAMED_UNIT ( * ) SI_UNIT ( $, .STERADIAN. ) SOLID_ANGLE_UNIT ( ) );
#1066=DIRECTION ( 'NONE',  ( 1.000000000000000000, 0.000000000000000000, 0.000000000000000000 ) ) ;
#1071=VERTEX_POINT ( 'NONE', #5602 ) ;
#1077=VERTEX_POINT ( 'NONE', #4942 ) ;
#1083=CARTESIAN_POINT ( 'NONE',  ( 44.00000000000009948, 13.41640786499835514, -95.00000000000000000 ) ) ;
#1084=AXIS2_PLACEMENT_3D ( 'NONE', #242, #181, #1197 ) ;
#1085=CARTESIAN_POINT ( 'NONE',  ( 0.000000000000000000, 0.000000000000000000, 23.00000000000000000 ) ) ;
#1086=DIRECTION ( 'NONE',  ( -0.000000000000000000, -0.000000000000000000, 1.000000000000000000 ) ) ;
#1088=CIRCLE ( 'NONE', #2849, 89.87058297576894006 ) ;
#1090=CARTESIAN_POINT ( 'NONE',  ( -15.82602517378898987, 37.28747423195201094, -225.0000000000000000 ) ) ;
#1093=DIRECTION ( 'NONE',  ( 1.000000000000000000, 0.000000000000000000, 0.000000000000000000 ) ) ;
#1097=AXIS2_PLACEMENT_3D ( 'NONE', #2904, #3422, #5977 ) ;
#1100=CARTESIAN_POINT ( 'NONE',  ( 44.00000000000009948, 13.41640786499835514, -115.0000000000000000 ) ) ;
#1103=FACE_OUTER_BOUND ( 'NONE', #1354, .T. ) ;
#1107=ORIENTED_EDGE ( 'NONE', *, *, #5044, .F. ) ;
#1112=AXIS2_PLACEMENT_3D ( 'NONE', #3105, #5591, #1757 ) ;
#1115=CIRCLE ( 'NONE', #1850, 17.00000000000000000 ) ;
#1117=LINE ( 'NONE', #2181, #4695 ) ;
#1119=DIRECTION ( 'NONE',  ( -0.000000000000000000, -0.000000000000000000, 1.000000000000000000 ) ) ;
#1130=ORIENTED_EDGE ( 'NONE', *, *, #517, .F. ) ;
#1131=EDGE_LOOP ( 'NONE', ( #2914, #3327, #1369, #3217 ) ) ;
#1133=FACE_BOUND ( 'NONE', #3515, .T. ) ;
#1136=CYLINDRICAL_SURFACE ( 'NONE', #1240, 90.00000000000319744 ) ;
#1137=ADVANCED_FACE ( 'NONE', ( #165 ), #539, .T. ) ;
#1142=CYLINDRICAL_SURFACE ( 'NONE', #15, 46.00000000000000000 ) ;
#1148=EDGE_CURVE ( 'NONE', #5556, #161, #4641, .T. ) ;
#1152=ORIENTED_EDGE ( 'NONE', *, *, #3889, .F. ) ;
#1153=CARTESIAN_POINT ( 'NONE',  ( 0.000000000000000000, 0.000000000000000000, 48.00000000000000000 ) ) ;
#1155=ADVANCED_FACE ( 'NONE', ( #3600 ), #3489, .T. ) ;
#1159=LINE ( 'NONE', #1675, #2443 ) ;
#1160=DIRECTION ( 'NONE',  ( -1.000000000000000000, 0.000000000000000000, 0.000000000000000000 ) ) ;
#1161=ADVANCED_FACE ( 'NONE', ( #16, #1494 ), #4598, .F. ) ;
#1166=DIRECTION ( 'NONE',  ( 1.000000000000000000, 0.000000000000000000, 0.000000000000000000 ) ) ;
#1168=ADVANCED_FACE ( 'NONE', ( #4632 ), #716, .T. ) ;
#1169=DIRECTION ( 'NONE',  ( -0.000000000000000000, -0.000000000000000000, 1.000000000000000000 ) ) ;
#1171=ORIENTED_EDGE ( 'NONE', *, *, #1817, .F. ) ;
#1172=CARTESIAN_POINT ( 'NONE',  ( 44.00000000000008527, 13.41640786499836224, -65.00000000000000000 ) ) ;
#1173=ADVANCED_FACE ( 'NONE', ( #5428, #4453 ), #3970, .F. ) ;
#1179=CARTESIAN_POINT ( 'NONE',  ( 17.00000000000000000, 25.00000000000000000, -30.00000000000000000 ) ) ;
#1183=CYLINDRICAL_SURFACE ( 'NONE', #3807, 90.00000000000319744 ) ;
#1188=VECTOR ( 'NONE', #5383, 1000.000000000000000 ) ;
#1190=AXIS2_PLACEMENT_3D ( 'NONE', #4900, #5480, #2538 ) ;
#1193=ORIENTED_EDGE ( 'NONE', *, *, #5028, .F. ) ;
#1197=DIRECTION ( 'NONE',  ( -1.000000000000000000, 0.000000000000000000, 0.000000000000000000 ) ) ;
#1202=DIRECTION ( 'NONE',  ( 1.000000000000000000, 0.000000000000000000, 0.000000000000000000 ) ) ;
#1203=EDGE_LOOP ( 'NONE', ( #4069, #6270, #2552, #5687 ) ) ;
#1206=FACE_OUTER_BOUND ( 'NONE', #1693, .T. ) ;
#1210=STYLED_ITEM('',(#6398),#4438);
#1214=DIRECTION ( 'NONE',  ( 1.000000000000000000, 0.000000000000000000, 0.000000000000000000 ) ) ;
#1216=FACE_OUTER_BOUND ( 'NONE', #1398, .T. ) ;
#1232=EDGE_CURVE ( 'NONE', #5213, #306, #436, .T. ) ;
#1233=CYLINDRICAL_SURFACE ( 'NONE', #585, 45.99999999999997868 ) ;
#1234=DIRECTION ( 'NONE',  ( -1.000000000000000000, 0.000000000000000000, 0.000000000000000000 ) ) ;
#1238=DIRECTION ( 'NONE',  ( 0.000000000000000000, -0.000000000000000000, 1.000000000000000000 ) ) ;
#1240=AXIS2_PLACEMENT_3D ( 'NONE', #571, #24, #3103 ) ;
#1241=EDGE_CURVE ( 'NONE', #2333, #5017, #1659, .T. ) ;
#1245=DIRECTION ( 'NONE',  ( -1.000000000000000000, 0.000000000000000000, 0.000000000000000000 ) ) ;
#1246=EDGE_CURVE ( 'NONE', #3894, #3208, #1559, .T. ) ;
#1249=DIRECTION ( 'NONE',  ( 1.000000000000000000, 0.000000000000000000, 0.000000000000000000 ) ) ;
#1252=DIRECTION ( 'NONE',  ( -0.000000000000000000, -0.000000000000000000, -1.000000000000000000 ) ) ;
#1253=EDGE_CURVE ( 'NONE', #3554, #427, #1356, .T. ) ;
#1259=CARTESIAN_POINT ( 'NONE',  ( -3.061616997868383043E-15, -25.00000000000000000, -65.00000000000000000 ) ) ;
#1260=EDGE_CURVE ( 'NONE', #4309, #214, #4117, .T. ) ;
#1268=FACE_OUTER_BOUND ( 'NONE', #6072, .T. ) ;
#1269=CYLINDRICAL_SURFACE ( 'NONE', #5545, 22.67164836619070911 ) ;
#1272=LINE ( 'NONE', #3201, #2649 ) ;
#1273=VERTEX_POINT ( 'NONE', #1311 ) ;
#1277=DIRECTION ( 'NONE',  ( -1.000000000000000000, 0.000000000000000000, 0.000000000000000000 ) ) ;
#1280=( LENGTH_UNIT ( ) NAMED_UNIT ( * ) SI_UNIT ( .MILLI., .METRE. ) );
#1286=ORIENTED_EDGE ( 'NONE', *, *, #5161, .F. ) ;
#1288=DIRECTION ( 'NONE',  ( -0.000000000000000000, -0.000000000000000000, 1.000000000000000000 ) ) ;
#1298=CARTESIAN_POINT ( 'NONE',  ( -17.00000000000000000, 2.081899558550500280E-15, -110.0000000000000000 ) ) ;
#1311=CARTESIAN_POINT ( 'NONE',  ( 16.99999999999999645, -24.99999999999999645, -130.0000000000000000 ) ) ;
#1312=DIRECTION ( 'NONE',  ( -0.000000000000000000, -0.000000000000000000, -1.000000000000000000 ) ) ;
#1313=CIRCLE ( 'NONE', #6361, 45.99999999999997868 ) ;
#1315=ORIENTED_EDGE ( 'NONE', *, *, #1970, .F. ) ;
#1321=AXIS2_PLACEMENT_3D ( 'NONE', #396, #3836, #879 ) ;
#1324=DIRECTION ( 'NONE',  ( 1.000000000000000000, 0.000000000000000000, 0.000000000000000000 ) ) ;
#1326=EDGE_CURVE ( 'NONE', #3504, #453, #5168, .T. ) ;
#1328=ORIENTED_EDGE ( 'NONE', *, *, #3925, .T. ) ;
#1330=EDGE_CURVE ( 'NONE', #4113, #5536, #2383, .T. ) ;
#1334=CARTESIAN_POINT ( 'NONE',  ( 22.21770253897382474, 3.871672004622519037, -49.99999999999999289 ) ) ;
#1335=DIRECTION ( 'NONE',  ( -0.000000000000000000, -0.000000000000000000, 1.000000000000000000 ) ) ;
#1337=VECTOR ( 'NONE', #589, 1000.000000000000000 ) ;
#1338=VERTEX_POINT ( 'NONE', #4213 ) ;
#1339=VERTEX_POINT ( 'NONE', #5701 ) ;
#1340=ORIENTED_EDGE ( 'NONE', *, *, #3449, .T. ) ;
#1343=DIRECTION ( 'NONE',  ( -1.000000000000000000, 0.000000000000000000, 0.000000000000000000 ) ) ;
#1348=ORIENTED_EDGE ( 'NONE', *, *, #5078, .F. ) ;
#1351=DIRECTION ( 'NONE',  ( 1.000000000000000000, 0.000000000000000000, 0.000000000000000000 ) ) ;
#1354=EDGE_LOOP ( 'NONE', ( #5339, #5786 ) ) ;
#1356=CIRCLE ( 'NONE', #6300, 17.00000000000000000 ) ;
#1363=ORIENTED_EDGE ( 'NONE', *, *, #32, .F. ) ;
#1366=DIRECTION ( 'NONE',  ( -1.000000000000000000, 0.000000000000000000, 0.000000000000000000 ) ) ;
#1369=ORIENTED_EDGE ( 'NONE', *, *, #2653, .T. ) ;
#1370=ORIENTED_EDGE ( 'NONE', *, *, #3127, .F. ) ;
#1371=VECTOR ( 'NONE', #6131, 1000.000000000000000 ) ;
#1376=FACE_OUTER_BOUND ( 'NONE', #4087, .T. ) ;
#1378=CARTESIAN_POINT ( 'NONE',  ( -17.00000000000000000, 25.00000000000000000, -195.0000000000000000 ) ) ;
#1380=EDGE_LOOP ( 'NONE', ( #4030, #4690 ) ) ;
#1381=CARTESIAN_POINT ( 'NONE',  ( -16.23652742703190199, -37.28747423195189015, -175.0000000000000284 ) ) ;
#1382=CARTESIAN_POINT ( 'NONE',  ( -15.82602517378898987, 37.28747423195201094, 0.000000000000000000 ) ) ;
#1387=DIRECTION ( 'NONE',  ( -0.000000000000000000, -0.000000000000000000, -1.000000000000000000 ) ) ;
#1396=CARTESIAN_POINT ( 'NONE',  ( -17.00000000000000355, -24.99999999999999645, -65.00000000000000000 ) ) ;
#1398=EDGE_LOOP ( 'NONE', ( #2607, #2726, #1171, #805 ) ) ;
#1401=VECTOR ( 'NONE', #183, 1000.000000000000000 ) ;
#1402=FACE_OUTER_BOUND ( 'NONE', #4776, .T. ) ;
#1403=ADVANCED_FACE ( 'NONE', ( #2507, #3832 ), #2916, .F. ) ;
#1406=EDGE_CURVE ( 'NONE', #1569, #2268, #1480, .T. ) ;
#1410=ADVANCED_FACE ( 'NONE', ( #5803 ), #3891, .T. ) ;
#1419=DIRECTION ( 'NONE',  ( 0.000000000000000000, 0.000000000000000000, -1.000000000000000000 ) ) ;
#1424=ORIENTED_EDGE ( 'NONE', *, *, #1799, .F. ) ;
#1426=CIRCLE ( 'NONE', #5021, 46.00000000000000000 ) ;
#1427=CARTESIAN_POINT ( 'NONE',  ( 17.00000000000000000, 0.000000000000000000, -273.0000000000000000 ) ) ;
#1434=ORIENTED_EDGE ( 'NONE', *, *, #3467, .T. ) ;
#1437=AXIS2_PLACEMENT_3D ( 'NONE', #2023, #577, #5960 ) ;
#1445=CARTESIAN_POINT ( 'NONE',  ( -16.23652742703190199, -37.28747423195189015, -160.0000000000000284 ) ) ;
#1447=DIRECTION ( 'NONE',  ( -0.000000000000000000, -0.000000000000000000, 1.000000000000000000 ) ) ;
#1451=ORIENTED_EDGE ( 'NONE', *, *, #2077, .T. ) ;
#1452=EDGE_CURVE ( 'NONE', #2909, #4309, #2423, .T. ) ;
#1456=FACE_BOUND ( 'NONE', #2815, .T. ) ;
#1463=ORIENTED_EDGE ( 'NONE', *, *, #3449, .F. ) ;
#1466=CARTESIAN_POINT ( 'NONE',  ( -44.00000000000000000, -13.41640786499873172, -225.0000000000000000 ) ) ;
#1469=DIRECTION ( 'NONE',  ( 0.000000000000000000, 0.000000000000000000, -1.000000000000000000 ) ) ;
#1471=ORIENTED_EDGE ( 'NONE', *, *, #5559, .F. ) ;
#1475=AXIS2_PLACEMENT_3D ( 'NONE', #537, #5369, #3942 ) ;
#1478=DIRECTION ( 'NONE',  ( -1.000000000000000000, 0.000000000000000000, 0.000000000000000000 ) ) ;
#1480=LINE ( 'NONE', #4826, #994 ) ;
#1487=CARTESIAN_POINT ( 'NONE',  ( -19.00000000000000000, 0.000000000000000000, 23.00000000000000000 ) ) ;
#1488=VERTEX_POINT ( 'NONE', #5994 ) ;
#1494=FACE_BOUND ( 'NONE', #4888, .T. ) ;
#1496=LINE ( 'NONE', #4643, #102 ) ;
#1499=ORIENTED_EDGE ( 'NONE', *, *, #2188, .F. ) ;
#1501=VECTOR ( 'NONE', #1288, 1000.000000000000000 ) ;
#1502=DIRECTION ( 'NONE',  ( -0.000000000000000000, -0.000000000000000000, -1.000000000000000000 ) ) ;
#1503=VECTOR ( 'NONE', #4518, 1000.000000000000000 ) ;
#1516=CIRCLE ( 'NONE', #1012, 17.00000000000000000 ) ;
#1524=DIRECTION ( 'NONE',  ( 1.000000000000000000, 0.000000000000000000, 0.000000000000000000 ) ) ;
#1526=CARTESIAN_POINT ( 'NONE',  ( 16.23652742703164975, 37.28747423195200383, -30.00000000000000000 ) ) ;
#1528=VECTOR ( 'NONE', #1908, 1000.000000000000000 ) ;
#1532=AXIS2_PLACEMENT_3D ( 'NONE', #1153, #4570, #3186 ) ;
#1534=CARTESIAN_POINT ( 'NONE',  ( 0.000000000000000000, 0.000000000000000000, -115.0000000000000000 ) ) ;
#1537=VERTEX_POINT ( 'NONE', #3535 ) ;
#1538=VECTOR ( 'NONE', #993, 1000.000000000000000 ) ;
#1542=DIRECTION ( 'NONE',  ( -1.000000000000000000, 0.000000000000000000, 0.000000000000000000 ) ) ;
#1546=CARTESIAN_POINT ( 'NONE',  ( 0.000000000000000000, 0.000000000000000000, -225.0000000000000000 ) ) ;
#1557=VERTEX_POINT ( 'NONE', #4559 ) ;
#1558=ORIENTED_EDGE ( 'NONE', *, *, #3748, .T. ) ;
#1559=CIRCLE ( 'NONE', #4021, 89.87058297576894006 ) ;
#1561=DIRECTION ( 'NONE',  ( 1.000000000000000000, 0.000000000000000000, 0.000000000000000000 ) ) ;
#1563=DIRECTION ( 'NONE',  ( 1.000000000000000000, 0.000000000000000000, 0.000000000000000000 ) ) ;
#1564=ORIENTED_EDGE ( 'NONE', *, *, #5084, .T. ) ;
#1567=AXIS2_PLACEMENT_3D ( 'NONE', #5041, #4123, #2679 ) ;
#1569=VERTEX_POINT ( 'NONE', #2113 ) ;
#1570=ORIENTED_EDGE ( 'NONE', *, *, #968, .F. ) ;
#1571=CYLINDRICAL_SURFACE ( 'NONE', #2421, 46.00000000000000000 ) ;
#1573=FACE_BOUND ( 'NONE', #4746, .T. ) ;
#1578=CARTESIAN_POINT ( 'NONE',  ( 13.14183123006966980, -39.58265509608656174, -110.0000000000000000 ) ) ;
#1579=DIRECTION ( 'NONE',  ( -1.000000000000000000, 0.000000000000000000, 0.000000000000000000 ) ) ;
#1581=ORIENTED_EDGE ( 'NONE', *, *, #5069, .F. ) ;
#1583=CARTESIAN_POINT ( 'NONE',  ( 16.23652742703164620, 37.28747423195200383, -240.0000000000000000 ) ) ;
#1585=DIRECTION ( 'NONE',  ( 1.000000000000000000, 0.000000000000000000, 0.000000000000000000 ) ) ;
#1587=DIRECTION ( 'NONE',  ( -0.000000000000000000, -0.000000000000000000, 1.000000000000000000 ) ) ;
#1589=AXIS2_PLACEMENT_3D ( 'NONE', #907, #3935, #2999 ) ;
#1590=APPLICATION_CONTEXT ( 'automotive_design' ) ;
#1597=DIRECTION ( 'NONE',  ( -0.000000000000000000, -0.000000000000000000, 1.000000000000000000 ) ) ;
#1598=ORIENTED_EDGE ( 'NONE', *, *, #5920, .F. ) ;
#1599=ADVANCED_FACE ( 'NONE', ( #1206 ), #1690, .T. ) ;
#1601=VECTOR ( 'NONE', #5254, 1000.000000000000000 ) ;
#1603=AXIS2_PLACEMENT_3D ( 'NONE', #5398, #2810, #4811 ) ;
#1607=CIRCLE ( 'NONE', #2536, 17.00000000000000000 ) ;
#1609=DIRECTION ( 'NONE',  ( 1.000000000000000000, 0.000000000000000000, 0.000000000000000000 ) ) ;
#1612=EDGE_CURVE ( 'NONE', #3307, #2452, #3646, .T. ) ;
#1623=DIRECTION ( 'NONE',  ( 1.000000000000000000, 0.000000000000000000, 0.000000000000000000 ) ) ;
#1630=EDGE_CURVE ( 'NONE', #146, #1019, #5206, .T. ) ;
#1631=ORIENTED_EDGE ( 'NONE', *, *, #5363, .T. ) ;
#1635=AXIS2_PLACEMENT_3D ( 'NONE', #4782, #957, #6330 ) ;
#1641=AXIS2_PLACEMENT_3D ( 'NONE', #5918, #4975, #566 ) ;
#1643=ORIENTED_EDGE ( 'NONE', *, *, #2188, .T. ) ;
#1646=CIRCLE ( 'NONE', #422, 22.67164836619066648 ) ;
#1648=CARTESIAN_POINT ( 'NONE',  ( 16.23652742703164975, 37.28747423195200383, -180.0000000000000000 ) ) ;
#1651=ORIENTED_EDGE ( 'NONE', *, *, #2390, .T. ) ;
#1657=CARTESIAN_POINT ( 'NONE',  ( -43.99999999999990052, 13.41640786499905147, -65.00000000000000000 ) ) ;
#1659=CIRCLE ( 'NONE', #954, 89.87058297576894006 ) ;
#1660=FACE_OUTER_BOUND ( 'NONE', #2542, .T. ) ;
#1661=ORIENTED_EDGE ( 'NONE', *, *, #1892, .T. ) ;
#1664=CARTESIAN_POINT ( 'NONE',  ( -3.061616997868383043E-15, -25.00000000000000000, -95.00000000000000000 ) ) ;
#1669=DIRECTION ( 'NONE',  ( 1.000000000000000000, 0.000000000000000000, 0.000000000000000000 ) ) ;
#1670=ORIENTED_EDGE ( 'NONE', *, *, #875, .F. ) ;
#1672=CIRCLE ( 'NONE', #6103, 46.00000000000000000 ) ;
#1675=CARTESIAN_POINT ( 'NONE',  ( -44.00000000000000000, -13.41640786499873172, -240.0000000000000000 ) ) ;
#1676=CARTESIAN_POINT ( 'NONE',  ( 0.000000000000000000, 0.000000000000000000, -248.0000000000000000 ) ) ;
#1678=EDGE_LOOP ( 'NONE', ( #4173, #1315, #5073, #3645 ) ) ;
#1680=CARTESIAN_POINT ( 'NONE',  ( 17.00000000000000000, 2.081899558550500280E-15, 48.00000000000000000 ) ) ;
#1686=EDGE_LOOP ( 'NONE', ( #27, #4335, #3100, #3984 ) ) ;
#1688=DIRECTION ( 'NONE',  ( -0.000000000000000000, -0.000000000000000000, -1.000000000000000000 ) ) ;
#1690=CYLINDRICAL_SURFACE ( 'NONE', #2622, 17.00000000000000000 ) ;
#1691=VERTEX_POINT ( 'NONE', #180 ) ;
#1693=EDGE_LOOP ( 'NONE', ( #4587, #2710, #3591, #147 ) ) ;
#1694=DIRECTION ( 'NONE',  ( -1.000000000000000000, 0.000000000000000000, 0.000000000000000000 ) ) ;
#1695=AXIS2_PLACEMENT_3D ( 'NONE', #2603, #2512, #5997 ) ;
#1698=ORIENTED_EDGE ( 'NONE', *, *, #1630, .F. ) ;
#1702=VECTOR ( 'NONE', #4647, 1000.000000000000000 ) ;
#1703=DIRECTION ( 'NONE',  ( -0.000000000000000000, -0.000000000000000000, 1.000000000000000000 ) ) ;
#1711=CARTESIAN_POINT ( 'NONE',  ( -16.23652742703190199, -37.28747423195189015, -160.0000000000000284 ) ) ;
#1712=CARTESIAN_POINT ( 'NONE',  ( -16.23652742703189489, -37.28747423195188304, -110.0000000000000000 ) ) ;
#1714=ADVANCED_FACE ( 'NONE', ( #3040 ), #3073, .T. ) ;
#1716=ORIENTED_EDGE ( 'NONE', *, *, #5697, .T. ) ;
#1717=CARTESIAN_POINT ( 'NONE',  ( -22.21770253897380343, -3.871672004622680241, -45.00000000000000000 ) ) ;
#1718=ORIENTED_EDGE ( 'NONE', *, *, #4181, .F. ) ;
#1719=AXIS2_PLACEMENT_3D ( 'NONE', #1717, #1238, #2004 ) ;
#1720=DIRECTION ( 'NONE',  ( -0.000000000000000000, -0.000000000000000000, -1.000000000000000000 ) ) ;
#1725=PRODUCT_DEFINITION ( 'UNKNOWN', '', #4254, #5671 ) ;
#1729=ADVANCED_FACE ( 'NONE', ( #1133, #2166 ), #6042, .T. ) ;
#1730=AXIS2_PLACEMENT_3D ( 'NONE', #5510, #5881, #3516 ) ;
#1731=EDGE_CURVE ( 'NONE', #4627, #4783, #4864, .T. ) ;
#1734=DIRECTION ( 'NONE',  ( 1.000000000000000000, 0.000000000000000000, 0.000000000000000000 ) ) ;
#1735=VECTOR ( 'NONE', #687, 1000.000000000000000 ) ;
#1742=VERTEX_POINT ( 'NONE', #6102 ) ;
#1745=CARTESIAN_POINT ( 'NONE',  ( -43.99999999999990052, 13.41640786499905147, -49.99999999999999289 ) ) ;
#1747=CIRCLE ( 'NONE', #1858, 17.00000000000000000 ) ;
#1748=DIRECTION ( 'NONE',  ( -0.000000000000000000, -0.000000000000000000, 1.000000000000000000 ) ) ;
#1750=EDGE_LOOP ( 'NONE', ( #789, #3524 ) ) ;
#1753=CARTESIAN_POINT ( 'NONE',  ( -44.43364355155666345, 29.42304313293565343, -160.0000000000000284 ) ) ;
#1754=AXIS2_PLACEMENT_3D ( 'NONE', #3517, #5484, #1066 ) ;
#1755=FACE_OUTER_BOUND ( 'NONE', #3252, .T. ) ;
#1756=CARTESIAN_POINT ( 'NONE',  ( 13.14183123006952947, -39.58265509608667543, -175.0000000000000284 ) ) ;
#1757=DIRECTION ( 'NONE',  ( 1.000000000000000000, 0.000000000000000000, 0.000000000000000000 ) ) ;
#1758=VERTEX_POINT ( 'NONE', #1680 ) ;
#1759=DIRECTION ( 'NONE',  ( -0.000000000000000000, -0.000000000000000000, -1.000000000000000000 ) ) ;
#1765=EDGE_LOOP ( 'NONE', ( #4569, #2233 ) ) ;
#1769=FACE_OUTER_BOUND ( 'NONE', #4542, .T. ) ;
#1770=CARTESIAN_POINT ( 'NONE',  ( 0.000000000000000000, 0.000000000000000000, -248.0000000000000000 ) ) ;
#1771=CARTESIAN_POINT ( 'NONE',  ( -22.21770253897380343, -3.871672004622680241, -180.0000000000000000 ) ) ;
#1775=LINE ( 'NONE', #5265, #3301 ) ;
#1777=LINE ( 'NONE', #5784, #5119 ) ;
#1778=VECTOR ( 'NONE', #4640, 1000.000000000000000 ) ;
#1784=DIRECTION ( 'NONE',  ( -0.000000000000000000, -0.000000000000000000, 1.000000000000000000 ) ) ;
#1787=EDGE_LOOP ( 'NONE', ( #1631, #1107, #285, #744 ) ) ;
#1790=DIRECTION ( 'NONE',  ( 1.000000000000000000, 0.000000000000000000, 0.000000000000000000 ) ) ;
#1796=DIRECTION ( 'NONE',  ( -0.000000000000000000, -0.000000000000000000, -1.000000000000000000 ) ) ;
#1797=ORIENTED_EDGE ( 'NONE', *, *, #1731, .T. ) ;
#1799=EDGE_CURVE ( 'NONE', #5724, #2249, #4712, .T. ) ;
#1806=ADVANCED_FACE ( 'NONE', ( #6164 ), #6201, .T. ) ;
#1817=EDGE_CURVE ( 'NONE', #4938, #4122, #2289, .T. ) ;
#1818=ORIENTED_EDGE ( 'NONE', *, *, #4397, .F. ) ;
#1828=ORIENTED_EDGE ( 'NONE', *, *, #5315, .F. ) ;
#1831=EDGE_LOOP ( 'NONE', ( #6351, #5689, #2614, #5375 ) ) ;
#1833=DIRECTION ( 'NONE',  ( 1.000000000000000000, 0.000000000000000000, -0.000000000000000000 ) ) ;
#1837=CARTESIAN_POINT ( 'NONE',  ( 0.000000000000000000, 0.000000000000000000, -49.99999999999999289 ) ) ;
#1838=AXIS2_PLACEMENT_3D ( 'NONE', #87, #4586, #4492 ) ;
#1843=CARTESIAN_POINT ( 'NONE',  ( -44.64065620456893413, -28.99954194078699032, -180.0000000000000000 ) ) ;
#1849=VECTOR ( 'NONE', #153, 1000.000000000000000 ) ;
#1850=AXIS2_PLACEMENT_3D ( 'NONE', #2052, #4012, #4652 ) ;
#1858=AXIS2_PLACEMENT_3D ( 'NONE', #4991, #2417, #4935 ) ;
#1862=CARTESIAN_POINT ( 'NONE',  ( 0.2052511266213280505, 21.25619793154159964, -225.0000000000000000 ) ) ;
#1863=AXIS2_PLACEMENT_3D ( 'NONE', #1664, #2601, #4628 ) ;
#1868=ORIENTED_EDGE ( 'NONE', *, *, #5232, .T. ) ;
#1871=DIRECTION ( 'NONE',  ( 0.000000000000000000, 0.000000000000000000, -1.000000000000000000 ) ) ;
#1872=FACE_OUTER_BOUND ( 'NONE', #4882, .T. ) ;
#1875=DIRECTION ( 'NONE',  ( -1.000000000000000000, 0.000000000000000000, 0.000000000000000000 ) ) ;
#1876=CARTESIAN_POINT ( 'NONE',  ( -17.00000000000000000, 2.081899558550500280E-15, -45.00000000000000000 ) ) ;
#1879=CARTESIAN_POINT ( 'NONE',  ( -43.99999999999990052, 13.41640786499905147, -160.0000000000000284 ) ) ;
#1881=VERTEX_POINT ( 'NONE', #2006 ) ;
#1882=DIRECTION ( 'NONE',  ( 0.000000000000000000, 0.000000000000000000, -1.000000000000000000 ) ) ;
#1886=LINE ( 'NONE', #5301, #5789 ) ;
#1889=ORIENTED_EDGE ( 'NONE', *, *, #2548, .T. ) ;
#1890=ORIENTED_EDGE ( 'NONE', *, *, #5812, .T. ) ;
#1892=EDGE_CURVE ( 'NONE', #1339, #5491, #36, .T. ) ;
#1897=DIRECTION ( 'NONE',  ( 1.000000000000000000, 0.000000000000000000, 0.000000000000000000 ) ) ;
#1899=CARTESIAN_POINT ( 'NONE',  ( -17.00000000000000000, 25.00000000000000000, -195.0000000000000000 ) ) ;
#1902=CARTESIAN_POINT ( 'NONE',  ( -19.00000000000000000, 2.326828918379970970E-15, -240.0000000000000000 ) ) ;
#1904=CARTESIAN_POINT ( 'NONE',  ( 17.00000000000000000, 25.00000000000000000, -30.00000000000000000 ) ) ;
#1907=ADVANCED_FACE ( 'NONE', ( #4452 ), #6327, .T. ) ;
#1908=DIRECTION ( 'NONE',  ( -0.000000000000000000, -0.000000000000000000, -1.000000000000000000 ) ) ;
#1914=DIRECTION ( 'NONE',  ( 1.000000000000000000, 0.000000000000000000, 0.000000000000000000 ) ) ;
#1915=CARTESIAN_POINT ( 'NONE',  ( 44.00000000000008527, 13.41640786499836224, -49.99999999999999289 ) ) ;
#1916=ORIENTED_EDGE ( 'NONE', *, *, #5904, .F. ) ;
#1921=DIRECTION ( 'NONE',  ( 1.000000000000000000, 0.000000000000000000, 0.000000000000000000 ) ) ;
#1922=EDGE_CURVE ( 'NONE', #1071, #4348, #1672, .T. ) ;
#1923=CIRCLE ( 'NONE', #4500, 17.00000000000000000 ) ;
#1925=ORIENTED_EDGE ( 'NONE', *, *, #2923, .T. ) ;
#1926=ADVANCED_FACE ( 'NONE', ( #6156 ), #2672, .T. ) ;
#1933=DIRECTION ( 'NONE',  ( 1.000000000000000000, 0.000000000000000000, 0.000000000000000000 ) ) ;
#1942=DIRECTION ( 'NONE',  ( 1.000000000000000000, 0.000000000000000000, 0.000000000000000000 ) ) ;
#1947=DIRECTION ( 'NONE',  ( -0.000000000000000000, -0.000000000000000000, 1.000000000000000000 ) ) ;
#1950=CIRCLE ( 'NONE', #822, 90.00000000000000000 ) ;
#1951=DIRECTION ( 'NONE',  ( -0.000000000000000000, -0.000000000000000000, 1.000000000000000000 ) ) ;
#1953=VERTEX_POINT ( 'NONE', #2765 ) ;
#1954=ORIENTED_EDGE ( 'NONE', *, *, #3238, .F. ) ;
#1955=EDGE_LOOP ( 'NONE', ( #3744, #550, #5018, #3634 ) ) ;
#1957=DIRECTION ( 'NONE',  ( -0.000000000000000000, 0.000000000000000000, -1.000000000000000000 ) ) ;
#1958=CIRCLE ( 'NONE', #2667, 89.87058297576894006 ) ;
#1964=CIRCLE ( 'NONE', #1754, 90.00000000000319744 ) ;
#1968=FACE_OUTER_BOUND ( 'NONE', #2369, .T. ) ;
#1969=ORIENTED_EDGE ( 'NONE', *, *, #2109, .F. ) ;
#1970=EDGE_CURVE ( 'NONE', #6010, #3220, #6258, .T. ) ;
#1972=FACE_OUTER_BOUND ( 'NONE', #4062, .T. ) ;
#1976=DIRECTION ( 'NONE',  ( 0.000000000000000000, 0.000000000000000000, -1.000000000000000000 ) ) ;
#1977=ORIENTED_EDGE ( 'NONE', *, *, #4314, .T. ) ;
#1981=DIRECTION ( 'NONE',  ( 0.000000000000000000, 0.000000000000000000, 1.000000000000000000 ) ) ;
#1982=PLANE ( 'NONE',  #4918 ) ;
#1984=ORIENTED_EDGE ( 'NONE', *, *, #2469, .T. ) ;
#1989=AXIS2_PLACEMENT_3D ( 'NONE', #5106, #697, #4615 ) ;
#1995=VERTEX_POINT ( 'NONE', #4740 ) ;
#2000=EDGE_CURVE ( 'NONE', #2906, #3955, #6208, .T. ) ;
#2004=DIRECTION ( 'NONE',  ( 1.000000000000000000, 0.000000000000000000, -0.000000000000000000 ) ) ;
#2005=ORIENTED_EDGE ( 'NONE', *, *, #3343, .F. ) ;
#2006=CARTESIAN_POINT ( 'NONE',  ( -44.00000000000000000, -13.41640786499873172, 15.00000000000000000 ) ) ;
#2009=CARTESIAN_POINT ( 'NONE',  ( 19.00000000000000000, 2.326828918379970970E-15, 23.00000000000000000 ) ) ;
#2017=CARTESIAN_POINT ( 'NONE',  ( -2.385244779468109755E-15, -1.040834085586084257E-14, -115.0000000000000000 ) ) ;
#2021=AXIS2_PLACEMENT_3D ( 'NONE', #1334, #3871, #4847 ) ;
#2023=CARTESIAN_POINT ( 'NONE',  ( -44.64065620456596406, -28.99954194078535963, -225.0000000000000000 ) ) ;
#2024=CARTESIAN_POINT ( 'NONE',  ( -0.2052511266214760433, -21.25619793154163517, -49.99999999999999289 ) ) ;
#2026=DIRECTION ( 'NONE',  ( -0.000000000000000000, -0.000000000000000000, -1.000000000000000000 ) ) ;
#2032=CIRCLE ( 'NONE', #4494, 19.00000000000000000 ) ;
#2034=VERTEX_POINT ( 'NONE', #262 ) ;
#2046=CARTESIAN_POINT ( 'NONE',  ( 44.00000000000008527, 13.41640786499836224, -160.0000000000000284 ) ) ;
#2048=AXIS2_PLACEMENT_3D ( 'NONE', #3818, #5792, #4257 ) ;
#2049=CYLINDRICAL_SURFACE ( 'NONE', #5959, 90.00000000000318323 ) ;
#2051=AXIS2_PLACEMENT_3D ( 'NONE', #4987, #1003, #3477 ) ;
#2052=CARTESIAN_POINT ( 'NONE',  ( 0.000000000000000000, 0.000000000000000000, -110.0000000000000000 ) ) ;
#2056=DIRECTION ( 'NONE',  ( -0.000000000000000000, -0.000000000000000000, -1.000000000000000000 ) ) ;
#2064=ORIENTED_EDGE ( 'NONE', *, *, #1058, .F. ) ;
#2069=DIRECTION ( 'NONE',  ( 1.000000000000000000, 0.000000000000000000, 0.000000000000000000 ) ) ;
#2070=CYLINDRICAL_SURFACE ( 'NONE', #5040, 19.00000000000000000 ) ;
#2077=EDGE_CURVE ( 'NONE', #1953, #1273, #2903, .T. ) ;
#2078=DIRECTION ( 'NONE',  ( 1.000000000000000000, 0.000000000000000000, 0.000000000000000000 ) ) ;
#2082=EDGE_CURVE ( 'NONE', #2034, #1488, #4773, .T. ) ;
#2087=AXIS2_PLACEMENT_3D ( 'NONE', #1753, #3719, #5683 ) ;
#2088=CYLINDRICAL_SURFACE ( 'NONE', #1863, 17.00000000000000000 ) ;
#2092=FACE_OUTER_BOUND ( 'NONE', #1056, .T. ) ;
#2093=ORIENTED_EDGE ( 'NONE', *, *, #2109, .T. ) ;
#2101=ORIENTED_EDGE ( 'NONE', *, *, #6012, .T. ) ;
#2103=ADVANCED_FACE ( 'NONE', ( #2728 ), #4705, .T. ) ;
#2105=FACE_OUTER_BOUND ( 'NONE', #2171, .T. ) ;
#2107=DIRECTION ( 'NONE',  ( -0.000000000000000000, -0.000000000000000000, -1.000000000000000000 ) ) ;
#2109=EDGE_CURVE ( 'NONE', #3061, #1339, #3747, .T. ) ;
#2110=CIRCLE ( 'NONE', #5721, 17.00000000000000000 ) ;
#2113=CARTESIAN_POINT ( 'NONE',  ( -17.00000000000000000, 2.081899558550500280E-15, -49.99999999999999289 ) ) ;
#2115=LINE ( 'NONE', #3656, #4215 ) ;
#2116=EDGE_LOOP ( 'NONE', ( #134, #3194, #4226, #6055 ) ) ;
#2119=DIRECTION ( 'NONE',  ( -0.000000000000000000, -0.000000000000000000, 1.000000000000000000 ) ) ;
#2129=ORIENTED_EDGE ( 'NONE', *, *, #1246, .T. ) ;
#2133=LINE ( 'NONE', #217, #1702 ) ;
#2135=CIRCLE ( 'NONE', #5129, 19.00000000000000000 ) ;
#2137=PLANE ( 'NONE',  #1838 ) ;
#2138=EDGE_LOOP ( 'NONE', ( #2348, #5071, #3428, #469 ) ) ;
#2145=PRODUCT ( 'Part 32,3_Varsay\X2\0131\X0\lan', 'Part 32,3_Varsay\X2\0131\X0\lan', '', ( #5566 ) ) ;
#2146=FACE_OUTER_BOUND ( 'NONE', #1203, .T. ) ;
#2147=EDGE_LOOP ( 'NONE', ( #3419, #5932 ) ) ;
#2149=CARTESIAN_POINT ( 'NONE',  ( -44.64065620456893413, -28.99954194078699032, -45.00000000000000000 ) ) ;
#2153=CARTESIAN_POINT ( 'NONE',  ( 44.64065620456912598, 28.99954194078667413, -65.00000000000000000 ) ) ;
#2155=CARTESIAN_POINT ( 'NONE',  ( -16.23652742703190199, -37.28747423195189015, -65.00000000000000000 ) ) ;
#2156=CARTESIAN_POINT ( 'NONE',  ( 17.00000000000000000, 2.081899558550500280E-15, -175.0000000000000284 ) ) ;
#2161=CIRCLE ( 'NONE', #3191, 90.00000000000321165 ) ;
#2164=ORIENTED_EDGE ( 'NONE', *, *, #3324, .T. ) ;
#2166=FACE_OUTER_BOUND ( 'NONE', #2361, .T. ) ;
#2167=CARTESIAN_POINT ( 'NONE',  ( 13.14183123006966980, -39.58265509608656174, -110.0000000000000000 ) ) ;
#2170=CARTESIAN_POINT ( 'NONE',  ( 44.43364355155687662, -29.42304313293534790, -30.00000000000000000 ) ) ;
#2171=EDGE_LOOP ( 'NONE', ( #1130, #2064, #6240, #4396 ) ) ;
#2177=CARTESIAN_POINT ( 'NONE',  ( 0.000000000000000000, 0.000000000000000000, -180.0000000000000000 ) ) ;
#2180=ADVANCED_FACE ( 'NONE', ( #4445 ), #2415, .T. ) ;
#2181=CARTESIAN_POINT ( 'NONE',  ( -17.00000000000000355, -25.00000000000000000, -130.0000000000000000 ) ) ;
#2188=EDGE_CURVE ( 'NONE', #3554, #4831, #3344, .T. ) ;
#2194=DIRECTION ( 'NONE',  ( -0.000000000000000000, -0.000000000000000000, 1.000000000000000000 ) ) ;
#2198=LINE ( 'NONE', #1657, #5865 ) ;
#2200=EDGE_LOOP ( 'NONE', ( #6112, #2449, #1564, #4036 ) ) ;
#2201=FACE_BOUND ( 'NONE', #3099, .T. ) ;
#2203=EDGE_CURVE ( 'NONE', #3504, #5509, #3863, .T. ) ;
#2206=VERTEX_POINT ( 'NONE', #1902 ) ;
#2207=LINE ( 'NONE', #2751, #9 ) ;
#2208=EDGE_LOOP ( 'NONE', ( #1463, #4499, #5951, #250 ) ) ;
#2210=CARTESIAN_POINT ( 'NONE',  ( 0.2052511266213299934, 21.25619793154162807, -30.00000000000000000 ) ) ;
#2211=AXIS2_PLACEMENT_3D ( 'NONE', #5841, #530, #2827 ) ;
#2214=ORIENTED_EDGE ( 'NONE', *, *, #1817, .T. ) ;
#2216=EDGE_LOOP ( 'NONE', ( #922, #2510, #570, #4157 ) ) ;
#2218=CARTESIAN_POINT ( 'NONE',  ( -3.061616997868383043E-15, -25.00000000000000000, -130.0000000000000000 ) ) ;
#2220=CIRCLE ( 'NONE', #2528, 90.00000000000000000 ) ;
#2221=CIRCLE ( 'NONE', #1190, 46.00000000000000000 ) ;
#2223=EDGE_LOOP ( 'NONE', ( #4071, #840 ) ) ;
#2227=PLANE ( 'NONE',  #5322 ) ;
#2228=CARTESIAN_POINT ( 'NONE',  ( 44.43364355155687662, -29.42304313293534790, -180.0000000000000000 ) ) ;
#2229=LINE ( 'NONE', #2618, #6069 ) ;
#2232=DIRECTION ( 'NONE',  ( 1.000000000000000000, 0.000000000000000000, 0.000000000000000000 ) ) ;
#2233=ORIENTED_EDGE ( 'NONE', *, *, #2390, .F. ) ;
#2237=CARTESIAN_POINT ( 'NONE',  ( -2.385244779468109755E-15, -1.040834085586084257E-14, -115.0000000000000000 ) ) ;
#2241=UNCERTAINTY_MEASURE_WITH_UNIT (LENGTH_MEASURE( 1.000000000000000082E-05 ), #3940, 'distance_accuracy_value', 'NONE');
#2242=DIRECTION ( 'NONE',  ( 0.000000000000000000, 0.000000000000000000, 1.000000000000000000 ) ) ;
#2249=VERTEX_POINT ( 'NONE', #1382 ) ;
#2252=DIRECTION ( 'NONE',  ( -0.000000000000000000, -0.000000000000000000, -1.000000000000000000 ) ) ;
#2257=ADVANCED_FACE ( 'NONE', ( #1972 ), #4834, .T. ) ;
#2259=VECTOR ( 'NONE', #2026, 1000.000000000000000 ) ;
#2262=DIRECTION ( 'NONE',  ( 1.000000000000000000, 0.000000000000000000, 0.000000000000000000 ) ) ;
#2264=CARTESIAN_POINT ( 'NONE',  ( -44.64065620456596406, -28.99954194078535963, -240.0000000000000000 ) ) ;
#2267=ADVANCED_FACE ( 'NONE', ( #1456, #3962 ), #7, .T. ) ;
#2268=VERTEX_POINT ( 'NONE', #1876 ) ;
#2270=ADVANCED_FACE ( 'NONE', ( #5936 ), #5361, .T. ) ;
#2271=EDGE_CURVE ( 'NONE', #1019, #686, #2621, .T. ) ;
#2277=CYLINDRICAL_SURFACE ( 'NONE', #3146, 17.00000000000000000 ) ;
#2281=FACE_OUTER_BOUND ( 'NONE', #1131, .T. ) ;
#2284=DIRECTION ( 'NONE',  ( 0.000000000000000000, 0.000000000000000000, 1.000000000000000000 ) ) ;
#2289=CIRCLE ( 'NONE', #1475, 17.00000000000000000 ) ;
#2292=ORIENTED_EDGE ( 'NONE', *, *, #1612, .F. ) ;
#2295=LINE ( 'NONE', #2394, #3145 ) ;
#2296=DIRECTION ( 'NONE',  ( 0.000000000000000000, 0.000000000000000000, 1.000000000000000000 ) ) ;
#2297=CYLINDRICAL_SURFACE ( 'NONE', #2048, 17.00000000000000000 ) ;
#2304=DIRECTION ( 'NONE',  ( -1.000000000000000000, 0.000000000000000000, 0.000000000000000000 ) ) ;
#2308=ORIENTED_EDGE ( 'NONE', *, *, #3611, .T. ) ;
#2309=ADVANCED_FACE ( 'NONE', ( #620 ), #1571, .T. ) ;
#2310=EDGE_CURVE ( 'NONE', #3367, #981, #5204, .T. ) ;
#2312=DIRECTION ( 'NONE',  ( 0.000000000000000000, 0.000000000000000000, -1.000000000000000000 ) ) ;
#2315=ADVANCED_FACE ( 'NONE', ( #5479 ), #4108, .T. ) ;
#2323=DIRECTION ( 'NONE',  ( -1.000000000000000000, 0.000000000000000000, 0.000000000000000000 ) ) ;
#2325=ORIENTED_EDGE ( 'NONE', *, *, #2353, .T. ) ;
#2326=EDGE_LOOP ( 'NONE', ( #3283, #239 ) ) ;
#2331=FACE_OUTER_BOUND ( 'NONE', #2698, .T. ) ;
#2332=DIRECTION ( 'NONE',  ( -0.000000000000000000, -0.000000000000000000, -1.000000000000000000 ) ) ;
#2333=VERTEX_POINT ( 'NONE', #1083 ) ;
#2335=CIRCLE ( 'NONE', #4592, 89.87058297576892585 ) ;
#2336=VERTEX_POINT ( 'NONE', #3115 ) ;
#2338=DIRECTION ( 'NONE',  ( -0.000000000000000000, -0.000000000000000000, -1.000000000000000000 ) ) ;
#2342=VECTOR ( 'NONE', #3865, 1000.000000000000000 ) ;
#2346=VECTOR ( 'NONE', #1759, 1000.000000000000000 ) ;
#2348=ORIENTED_EDGE ( 'NONE', *, *, #3619, .F. ) ;
#2352=CIRCLE ( 'NONE', #5962, 22.67164836619070911 ) ;
#2353=EDGE_CURVE ( 'NONE', #3234, #4844, #2929, .T. ) ;
#2358=ORIENTED_EDGE ( 'NONE', *, *, #3393, .T. ) ;
#2361=EDGE_LOOP ( 'NONE', ( #6122, #5009, #4149, #3249 ) ) ;
#2367=AXIS2_PLACEMENT_3D ( 'NONE', #839, #3794, #2818 ) ;
#2369=EDGE_LOOP ( 'NONE', ( #1828, #45, #1716, #2292 ) ) ;
#2371=CIRCLE ( 'NONE', #4845, 22.67164836619070911 ) ;
#2378=DIRECTION ( 'NONE',  ( -0.000000000000000000, 0.000000000000000000, -1.000000000000000000 ) ) ;
#2379=APPLICATION_CONTEXT ( 'automotive_design' ) ;
#2383=CIRCLE ( 'NONE', #5380, 22.67164836619068424 ) ;
#2389=CARTESIAN_POINT ( 'NONE',  ( 44.00000000000000000, -13.41640786499874771, 15.00000000000000000 ) ) ;
#2390=EDGE_CURVE ( 'NONE', #1273, #1953, #2110, .T. ) ;
#2393=EDGE_CURVE ( 'NONE', #624, #6099, #992, .T. ) ;
#2394=CARTESIAN_POINT ( 'NONE',  ( -17.00000000000000000, 2.081899558550500280E-15, -273.0000000000000000 ) ) ;
#2399=ORIENTED_EDGE ( 'NONE', *, *, #4211, .F. ) ;
#2400=ORIENTED_EDGE ( 'NONE', *, *, #1406, .T. ) ;
#2401=EDGE_CURVE ( 'NONE', #6280, #4815, #5212, .T. ) ;
#2404=ADVANCED_FACE ( 'NONE', ( #1769 ), #2277, .T. ) ;
#2407=ORIENTED_EDGE ( 'NONE', *, *, #3338, .T. ) ;
#2408=DIRECTION ( 'NONE',  ( -0.000000000000000000, -0.000000000000000000, -1.000000000000000000 ) ) ;
#2411=DIRECTION ( 'NONE',  ( 1.000000000000000000, 0.000000000000000000, 0.000000000000000000 ) ) ;
#2415=CYLINDRICAL_SURFACE ( 'NONE', #60, 17.00000000000000000 ) ;
#2417=DIRECTION ( 'NONE',  ( -0.000000000000000000, -0.000000000000000000, -1.000000000000000000 ) ) ;
#2418=ORIENTED_EDGE ( 'NONE', *, *, #2673, .F. ) ;
#2421=AXIS2_PLACEMENT_3D ( 'NONE', #4471, #3568, #4597 ) ;
#2423=CIRCLE ( 'NONE', #5415, 22.67164836619067714 ) ;
#2426=DIRECTION ( 'NONE',  ( -0.000000000000000000, -0.000000000000000000, -1.000000000000000000 ) ) ;
#2427=ORIENTED_EDGE ( 'NONE', *, *, #968, .T. ) ;
#2438=CARTESIAN_POINT ( 'NONE',  ( 0.000000000000000000, 0.000000000000000000, 15.00000000000000000 ) ) ;
#2442=CARTESIAN_POINT ( 'NONE',  ( 2.380270672502711906E-15, -5.204170427930421283E-15, -180.0000000000000000 ) ) ;
#2443=VECTOR ( 'NONE', #1703, 1000.000000000000000 ) ;
#2444=DIRECTION ( 'NONE',  ( -1.000000000000000000, 0.000000000000000000, 0.000000000000000000 ) ) ;
#2449=ORIENTED_EDGE ( 'NONE', *, *, #2082, .F. ) ;
#2452=VERTEX_POINT ( 'NONE', #4630 ) ;
#2454=DIRECTION ( 'NONE',  ( 0.000000000000000000, 0.000000000000000000, -1.000000000000000000 ) ) ;
#2455=LINE ( 'NONE', #1578, #5012 ) ;
#2456=CIRCLE ( 'NONE', #2975, 17.00000000000000000 ) ;
#2464=EDGE_CURVE ( 'NONE', #5105, #4627, #5637, .T. ) ;
#2469=EDGE_CURVE ( 'NONE', #5596, #3088, #2944, .T. ) ;
#2472=EDGE_CURVE ( 'NONE', #2613, #1537, #4799, .T. ) ;
#2479=DIRECTION ( 'NONE',  ( 1.000000000000000000, 0.000000000000000000, 0.000000000000000000 ) ) ;
#2483=EDGE_CURVE ( 'NONE', #602, #3628, #2835, .T. ) ;
#2486=CARTESIAN_POINT ( 'NONE',  ( -44.64065620456596406, -28.99954194078535963, -240.0000000000000000 ) ) ;
#2493=DIRECTION ( 'NONE',  ( 1.000000000000000000, 0.000000000000000000, 0.000000000000000000 ) ) ;
#2495=ORIENTED_EDGE ( 'NONE', *, *, #4184, .F. ) ;
#2496=ORIENTED_EDGE ( 'NONE', *, *, #4314, .F. ) ;
#2498=VERTEX_POINT ( 'NONE', #1179 ) ;
#2502=AXIS2_PLACEMENT_3D ( 'NONE', #1259, #236, #3805 ) ;
#2505=ADVANCED_FACE ( 'NONE', ( #2915 ), #3888, .T. ) ;
#2506=DIRECTION ( 'NONE',  ( -0.000000000000000000, -0.000000000000000000, 1.000000000000000000 ) ) ;
#2507=FACE_OUTER_BOUND ( 'NONE', #441, .T. ) ;
#2509=CYLINDRICAL_SURFACE ( 'NONE', #628, 90.00000000000000000 ) ;
#2510=ORIENTED_EDGE ( 'NONE', *, *, #1452, .F. ) ;
#2511=DIRECTION ( 'NONE',  ( -1.000000000000000000, 0.000000000000000000, 0.000000000000000000 ) ) ;
#2512=DIRECTION ( 'NONE',  ( -0.000000000000000000, -0.000000000000000000, 1.000000000000000000 ) ) ;
#2518=DIRECTION ( 'NONE',  ( -0.000000000000000000, -0.000000000000000000, -1.000000000000000000 ) ) ;
#2519=CARTESIAN_POINT ( 'NONE',  ( 16.99999999999999645, -24.99999999999999645, -130.0000000000000000 ) ) ;
#2522=CARTESIAN_POINT ( 'NONE',  ( 16.23652742703164975, 37.28747423195200383, -45.00000000000000000 ) ) ;
#2524=LINE ( 'NONE', #3042, #1538 ) ;
#2526=ORIENTED_EDGE ( 'NONE', *, *, #1799, .T. ) ;
#2528=AXIS2_PLACEMENT_3D ( 'NONE', #998, #5897, #4406 ) ;
#2534=ORIENTED_EDGE ( 'NONE', *, *, #3343, .T. ) ;
#2536=AXIS2_PLACEMENT_3D ( 'NONE', #1837, #3799, #2559 ) ;
#2537=DIRECTION ( 'NONE',  ( -1.000000000000000000, 0.000000000000000000, 0.000000000000000000 ) ) ;
#2538=DIRECTION ( 'NONE',  ( -1.000000000000000000, 0.000000000000000000, 0.000000000000000000 ) ) ;
#2541=CARTESIAN_POINT ( 'NONE',  ( 2.380270672502711906E-15, -5.204170427930421283E-15, -45.00000000000000000 ) ) ;
#2542=EDGE_LOOP ( 'NONE', ( #2907, #253, #4729, #2586 ) ) ;
#2548=EDGE_CURVE ( 'NONE', #4328, #1077, #2220, .T. ) ;
#2552=ORIENTED_EDGE ( 'NONE', *, *, #4011, .T. ) ;
#2556=CIRCLE ( 'NONE', #3375, 90.00000000000321165 ) ;
#2557=DIRECTION ( 'NONE',  ( -0.000000000000000000, -0.000000000000000000, -1.000000000000000000 ) ) ;
#2559=DIRECTION ( 'NONE',  ( -1.000000000000000000, 0.000000000000000000, 0.000000000000000000 ) ) ;
#2560=DIRECTION ( 'NONE',  ( -0.000000000000000000, -0.000000000000000000, -1.000000000000000000 ) ) ;
#2563=AXIS2_PLACEMENT_3D ( 'NONE', #4050, #5610, #788 ) ;
#2569=DIRECTION ( 'NONE',  ( 0.000000000000000000, 0.000000000000000000, -1.000000000000000000 ) ) ;
#2570=EDGE_CURVE ( 'NONE', #1537, #2613, #5420, .T. ) ;
#2571=DIRECTION ( 'NONE',  ( -0.000000000000000000, -0.000000000000000000, -1.000000000000000000 ) ) ;
#2572=DIRECTION ( 'NONE',  ( -0.000000000000000000, -0.000000000000000000, 1.000000000000000000 ) ) ;
#2577=EDGE_CURVE ( 'NONE', #2747, #1569, #3463, .T. ) ;
#2581=FACE_OUTER_BOUND ( 'NONE', #4107, .T. ) ;
#2586=ORIENTED_EDGE ( 'NONE', *, *, #2203, .F. ) ;
#2588=DIRECTION ( 'NONE',  ( 1.000000000000000000, 0.000000000000000000, 0.000000000000000000 ) ) ;
#2589=CYLINDRICAL_SURFACE ( 'NONE', #6186, 17.00000000000000000 ) ;
#2590=CARTESIAN_POINT ( 'NONE',  ( 0.000000000000000000, 0.000000000000000000, 23.00000000000000000 ) ) ;
#2591=EDGE_CURVE ( 'NONE', #713, #4635, #6338, .T. ) ;
#2597=ADVANCED_FACE ( 'NONE', ( #1376 ), #3335, .T. ) ;
#2601=DIRECTION ( 'NONE',  ( -0.000000000000000000, -0.000000000000000000, 1.000000000000000000 ) ) ;
#2603=CARTESIAN_POINT ( 'NONE',  ( -44.64065620456893413, -28.99954194078699032, -45.00000000000000000 ) ) ;
#2605=DIRECTION ( 'NONE',  ( -0.000000000000000000, -0.000000000000000000, -1.000000000000000000 ) ) ;
#2606=FACE_OUTER_BOUND ( 'NONE', #2643, .T. ) ;
#2607=ORIENTED_EDGE ( 'NONE', *, *, #2401, .T. ) ;
#2613=VERTEX_POINT ( 'NONE', #423 ) ;
#2614=ORIENTED_EDGE ( 'NONE', *, *, #5232, .F. ) ;
#2618=CARTESIAN_POINT ( 'NONE',  ( -17.00000000000000000, 0.000000000000000000, -175.0000000000000000 ) ) ;
#2621=CIRCLE ( 'NONE', #3241, 46.00000000000000000 ) ;
#2622=AXIS2_PLACEMENT_3D ( 'NONE', #4723, #4235, #2304 ) ;
#2625=ADVANCED_FACE ( 'NONE', ( #5831, #457 ), #3927, .T. ) ;
#2626=ORIENTED_EDGE ( 'NONE', *, *, #2673, .T. ) ;
#2639=AXIS2_PLACEMENT_3D ( 'NONE', #4356, #1784, #3756 ) ;
#2641=FACE_OUTER_BOUND ( 'NONE', #6287, .T. ) ;
#2642=ORIENTED_EDGE ( 'NONE', *, *, #2662, .T. ) ;
#2643=EDGE_LOOP ( 'NONE', ( #4329, #5714, #1370, #4459 ) ) ;
#2644=ORIENTED_EDGE ( 'NONE', *, *, #2353, .F. ) ;
#2647=CARTESIAN_POINT ( 'NONE',  ( 22.21770253897382474, 3.871672004622519037, -175.0000000000000284 ) ) ;
#2648=DIRECTION ( 'NONE',  ( 1.000000000000000000, 0.000000000000000000, 0.000000000000000000 ) ) ;
#2649=VECTOR ( 'NONE', #1387, 1000.000000000000000 ) ;
#2650=CARTESIAN_POINT ( 'NONE',  ( 0.000000000000000000, 25.00000000000000000, -195.0000000000000000 ) ) ;
#2651=DIRECTION ( 'NONE',  ( 1.000000000000000000, 0.000000000000000000, 0.000000000000000000 ) ) ;
#2652=ORIENTED_EDGE ( 'NONE', *, *, #390, .T. ) ;
#2653=EDGE_CURVE ( 'NONE', #2747, #1338, #4269, .T. ) ;
#2654=DIRECTION ( 'NONE',  ( 0.000000000000000000, 0.000000000000000000, -1.000000000000000000 ) ) ;
#2661=ORIENTED_EDGE ( 'NONE', *, *, #3013, .T. ) ;
#2662=EDGE_CURVE ( 'NONE', #2995, #686, #5142, .T. ) ;
#2664=DIRECTION ( 'NONE',  ( -0.000000000000000000, -0.000000000000000000, -1.000000000000000000 ) ) ;
#2666=DIRECTION ( 'NONE',  ( 0.000000000000000000, 0.000000000000000000, 1.000000000000000000 ) ) ;
#2667=AXIS2_PLACEMENT_3D ( 'NONE', #1062, #3938, #3901 ) ;
#2672=CYLINDRICAL_SURFACE ( 'NONE', #4973, 90.00000000000322586 ) ;
#2673=EDGE_CURVE ( 'NONE', #4815, #6280, #4204, .T. ) ;
#2675=CIRCLE ( 'NONE', #6289, 22.67164836619070911 ) ;
#2678=ORIENTED_EDGE ( 'NONE', *, *, #2401, .F. ) ;
#2679=DIRECTION ( 'NONE',  ( 1.000000000000000000, 0.000000000000000000, 0.000000000000000000 ) ) ;
#2681=DIRECTION ( 'NONE',  ( 0.000000000000000000, 0.000000000000000000, 1.000000000000000000 ) ) ;
#2684=CARTESIAN_POINT ( 'NONE',  ( -2.385244779468109755E-15, -1.040834085586084257E-14, -130.0000000000000000 ) ) ;
#2686=DIRECTION ( 'NONE',  ( -0.000000000000000000, -0.000000000000000000, -1.000000000000000000 ) ) ;
#2691=CARTESIAN_POINT ( 'NONE',  ( 0.000000000000000000, 25.00000000000000000, -195.0000000000000000 ) ) ;
#2698=EDGE_LOOP ( 'NONE', ( #4968, #4895, #885, #1499 ) ) ;
#2704=ORIENTED_EDGE ( 'NONE', *, *, #5614, .F. ) ;
#2707=FACE_OUTER_BOUND ( 'NONE', #4912, .T. ) ;
#2708=DIRECTION ( 'NONE',  ( -0.000000000000000000, -0.000000000000000000, -1.000000000000000000 ) ) ;
#2709=CARTESIAN_POINT ( 'NONE',  ( 17.00000000000000000, 0.000000000000000000, -49.99999999999999289 ) ) ;
#2710=ORIENTED_EDGE ( 'NONE', *, *, #4153, .T. ) ;
#2712=ORIENTED_EDGE ( 'NONE', *, *, #390, .F. ) ;
#2713=DIRECTION ( 'NONE',  ( -1.000000000000000000, 0.000000000000000000, 0.000000000000000000 ) ) ;
#2717=ORIENTED_EDGE ( 'NONE', *, *, #3933, .T. ) ;
#2721=EDGE_CURVE ( 'NONE', #5017, #4627, #3490, .T. ) ;
#2722=CYLINDRICAL_SURFACE ( 'NONE', #3478, 46.00000000000000000 ) ;
#2723=DIRECTION ( 'NONE',  ( -0.000000000000000000, -0.000000000000000000, -1.000000000000000000 ) ) ;
#2726=ORIENTED_EDGE ( 'NONE', *, *, #3994, .T. ) ;
#2728=FACE_OUTER_BOUND ( 'NONE', #2200, .T. ) ;
#2731=DIRECTION ( 'NONE',  ( 1.000000000000000000, 0.000000000000000000, 0.000000000000000000 ) ) ;
#2733=LINE ( 'NONE', #5552, #5143 ) ;
#2738=ADVANCED_FACE ( 'NONE', ( #4156, #3683 ), #6134, .F. ) ;
#2742=CARTESIAN_POINT ( 'NONE',  ( 0.000000000000000000, 0.000000000000000000, 23.00000000000000000 ) ) ;
#2746=DIRECTION ( 'NONE',  ( -1.000000000000000000, 0.000000000000000000, 0.000000000000000000 ) ) ;
#2747=VERTEX_POINT ( 'NONE', #2709 ) ;
#2751=CARTESIAN_POINT ( 'NONE',  ( -13.14183123006980480, 39.58265509608657595, -45.00000000000000000 ) ) ;
#2752=ORIENTED_EDGE ( 'NONE', *, *, #1232, .T. ) ;
#2754=( NAMED_UNIT ( * ) PLANE_ANGLE_UNIT ( ) SI_UNIT ( $, .RADIAN. ) );
#2759=ORIENTED_EDGE ( 'NONE', *, *, #5833, .F. ) ;
#2763=EDGE_CURVE ( 'NONE', #5556, #1537, #2229, .T. ) ;
#2765=CARTESIAN_POINT ( 'NONE',  ( -17.00000000000000355, -25.00000000000000000, -130.0000000000000000 ) ) ;
#2766=CIRCLE ( 'NONE', #5360, 17.00000000000000000 ) ;
#2770=ORIENTED_EDGE ( 'NONE', *, *, #2203, .T. ) ;
#2771=EDGE_LOOP ( 'NONE', ( #3292, #1471, #1818, #2308 ) ) ;
#2777=DIRECTION ( 'NONE',  ( 1.000000000000000000, 0.000000000000000000, 0.000000000000000000 ) ) ;
#2778=ADVANCED_FACE ( 'NONE', ( #5205 ), #795, .T. ) ;
#2780=VERTEX_POINT ( 'NONE', #5563 ) ;
#2782=AXIS2_PLACEMENT_3D ( 'NONE', #926, #2880, #2078 ) ;
#2783=DIRECTION ( 'NONE',  ( -1.000000000000000000, 0.000000000000000000, 0.000000000000000000 ) ) ;
#2788=AXIS2_PLACEMENT_3D ( 'NONE', #5256, #2312, #391 ) ;
#2789=ADVANCED_BREP_SHAPE_REPRESENTATION ( '', ( #4438, #6349 ), #5524 ) ;
#2794=CARTESIAN_POINT ( 'NONE',  ( -0.2052511266214760433, -21.25619793154163517, -65.00000000000000000 ) ) ;
#2797=CARTESIAN_POINT ( 'NONE',  ( -17.00000000000000000, 0.000000000000000000, 48.00000000000000000 ) ) ;
#2799=ORIENTED_EDGE ( 'NONE', *, *, #588, .F. ) ;
#2803=DIRECTION ( 'NONE',  ( -1.000000000000000000, 0.000000000000000000, 0.000000000000000000 ) ) ;
#2810=DIRECTION ( 'NONE',  ( 0.000000000000000000, 0.000000000000000000, -1.000000000000000000 ) ) ;
#2811=FACE_OUTER_BOUND ( 'NONE', #3128, .T. ) ;
#2812=ADVANCED_FACE ( 'NONE', ( #5374, #5304 ), #889, .F. ) ;
#2815=EDGE_LOOP ( 'NONE', ( #2678, #2418 ) ) ;
#2816=DIRECTION ( 'NONE',  ( -0.000000000000000000, -0.000000000000000000, 1.000000000000000000 ) ) ;
#2818=DIRECTION ( 'NONE',  ( 1.000000000000000000, 0.000000000000000000, 0.000000000000000000 ) ) ;
#2824=ORIENTED_EDGE ( 'NONE', *, *, #5920, .T. ) ;
#2827=DIRECTION ( 'NONE',  ( 1.000000000000000000, 0.000000000000000000, 0.000000000000000000 ) ) ;
#2829=DIRECTION ( 'NONE',  ( 0.000000000000000000, 0.000000000000000000, -1.000000000000000000 ) ) ;
#2835=CIRCLE ( 'NONE', #6244, 22.67164836619070911 ) ;
#2836=DIRECTION ( 'NONE',  ( -0.000000000000000000, -0.000000000000000000, 1.000000000000000000 ) ) ;
#2838=CARTESIAN_POINT ( 'NONE',  ( 0.000000000000000000, 0.000000000000000000, 0.000000000000000000 ) ) ;
#2839=DIRECTION ( 'NONE',  ( 1.000000000000000000, 0.000000000000000000, 0.000000000000000000 ) ) ;
#2843=CARTESIAN_POINT ( 'NONE',  ( 17.00000000000000000, 0.000000000000000000, -110.0000000000000000 ) ) ;
#2844=AXIS2_PLACEMENT_3D ( 'NONE', #3995, #4974, #2493 ) ;
#2845=LINE ( 'NONE', #3733, #2881 ) ;
#2846=ORIENTED_EDGE ( 'NONE', *, *, #6209, .T. ) ;
#2849=AXIS2_PLACEMENT_3D ( 'NONE', #3899, #5878, #3182 ) ;
#2850=DIRECTION ( 'NONE',  ( -0.000000000000000000, -0.000000000000000000, -1.000000000000000000 ) ) ;
#2853=AXIS2_PLACEMENT_3D ( 'NONE', #3503, #3469, #3853 ) ;
#2854=DIRECTION ( 'NONE',  ( -0.000000000000000000, -0.000000000000000000, -1.000000000000000000 ) ) ;
#2865=VECTOR ( 'NONE', #3077, 1000.000000000000000 ) ;
#2867=EDGE_CURVE ( 'NONE', #157, #5299, #5867, .T. ) ;
#2871=VECTOR ( 'NONE', #685, 1000.000000000000000 ) ;
#2877=ORIENTED_EDGE ( 'NONE', *, *, #2271, .T. ) ;
#2880=DIRECTION ( 'NONE',  ( -0.000000000000000000, -0.000000000000000000, -1.000000000000000000 ) ) ;
#2881=VECTOR ( 'NONE', #4163, 1000.000000000000000 ) ;
#2882=CARTESIAN_POINT ( 'NONE',  ( 22.21770253897382474, 3.871672004622519037, -130.0000000000000000 ) ) ;
#2886=EDGE_LOOP ( 'NONE', ( #3789, #171, #4841, #4850 ) ) ;
#2894=AXIS2_PLACEMENT_3D ( 'NONE', #199, #1981, #4109 ) ;
#2898=VERTEX_POINT ( 'NONE', #1915 ) ;
#2900=ORIENTED_EDGE ( 'NONE', *, *, #4751, .T. ) ;
#2903=CIRCLE ( 'NONE', #3945, 17.00000000000000000 ) ;
#2904=CARTESIAN_POINT ( 'NONE',  ( -0.2052511266214760433, -21.25619793154163517, -110.0000000000000000 ) ) ;
#2906=VERTEX_POINT ( 'NONE', #1396 ) ;
#2907=ORIENTED_EDGE ( 'NONE', *, *, #1326, .T. ) ;
#2909=VERTEX_POINT ( 'NONE', #439 ) ;
#2914=ORIENTED_EDGE ( 'NONE', *, *, #1406, .F. ) ;
#2915=FACE_OUTER_BOUND ( 'NONE', #604, .T. ) ;
#2916=PLANE ( 'NONE',  #3768 ) ;
#2917=DIRECTION ( 'NONE',  ( -0.000000000000000000, -0.000000000000000000, -1.000000000000000000 ) ) ;
#2918=CARTESIAN_POINT ( 'NONE',  ( 44.56092774862622719, -29.44644455561813956, 15.00000000000000000 ) ) ;
#2923=EDGE_CURVE ( 'NONE', #542, #5184, #4621, .T. ) ;
#2924=LINE ( 'NONE', #3445, #2342 ) ;
#2929=CIRCLE ( 'NONE', #4892, 90.00000000000319744 ) ;
#2936=EDGE_CURVE ( 'NONE', #4613, #542, #6362, .T. ) ;
#2939=EDGE_LOOP ( 'NONE', ( #88, #2400, #447, #3377 ) ) ;
#2942=ADVANCED_FACE ( 'NONE', ( #346 ), #2297, .T. ) ;
#2944=CIRCLE ( 'NONE', #4487, 22.67164836619067714 ) ;
#2946=CARTESIAN_POINT ( 'NONE',  ( -19.00000000000000000, 2.326828918379970970E-15, -248.0000000000000000 ) ) ;
#2948=AXIS2_PLACEMENT_3D ( 'NONE', #126, #4338, #1623 ) ;
#2950=ORIENTED_EDGE ( 'NONE', *, *, #4355, .T. ) ;
#2951=ADVANCED_FACE ( 'NONE', ( #4391 ), #5279, .T. ) ;
#2953=DIRECTION ( 'NONE',  ( -0.000000000000000000, -0.000000000000000000, 1.000000000000000000 ) ) ;
#2958=CARTESIAN_POINT ( 'NONE',  ( 44.56092774862622719, -29.44644455561813956, -240.0000000000000000 ) ) ;
#2964=AXIS2_PLACEMENT_3D ( 'NONE', #3559, #4006, #2651 ) ;
#2968=ADVANCED_FACE ( 'NONE', ( #3910 ), #3423, .T. ) ;
#2971=CARTESIAN_POINT ( 'NONE',  ( 0.000000000000000000, 25.00000000000000000, 0.000000000000000000 ) ) ;
#2974=DIRECTION ( 'NONE',  ( 0.000000000000000000, -0.000000000000000000, 1.000000000000000000 ) ) ;
#2975=AXIS2_PLACEMENT_3D ( 'NONE', #55, #1957, #3953 ) ;
#2979=ORIENTED_EDGE ( 'NONE', *, *, #875, .T. ) ;
#2981=VECTOR ( 'NONE', #3493, 1000.000000000000000 ) ;
#2982=EDGE_CURVE ( 'NONE', #2206, #5509, #5768, .T. ) ;
#2989=AXIS2_PLACEMENT_3D ( 'NONE', #2958, #4497, #94 ) ;
#2990=CARTESIAN_POINT ( 'NONE',  ( 0.000000000000000000, 0.000000000000000000, -240.0000000000000000 ) ) ;
#2995=VERTEX_POINT ( 'NONE', #4456 ) ;
#2999=DIRECTION ( 'NONE',  ( -1.000000000000000000, 0.000000000000000000, 0.000000000000000000 ) ) ;
#3000=LINE ( 'NONE', #1006, #708 ) ;
#3001=AXIS2_PLACEMENT_3D ( 'NONE', #4907, #505, #4426 ) ;
#3003=EDGE_LOOP ( 'NONE', ( #5821, #6234 ) ) ;
#3007=DIRECTION ( 'NONE',  ( 1.000000000000000000, 0.000000000000000000, 0.000000000000000000 ) ) ;
#3010=ORIENTED_EDGE ( 'NONE', *, *, #3131, .F. ) ;
#3012=CYLINDRICAL_SURFACE ( 'NONE', #5838, 22.67164836619066648 ) ;
#3013=EDGE_CURVE ( 'NONE', #1273, #4284, #3457, .T. ) ;
#3015=DIRECTION ( 'NONE',  ( -1.000000000000000000, 0.000000000000000000, 0.000000000000000000 ) ) ;
#3022=CARTESIAN_POINT ( 'NONE',  ( -43.99999999999987921, 13.41640786499904969, -95.00000000000000000 ) ) ;
#3029=DIRECTION ( 'NONE',  ( -0.000000000000000000, -0.000000000000000000, 1.000000000000000000 ) ) ;
#3031=DIRECTION ( 'NONE',  ( -0.000000000000000000, -0.000000000000000000, 1.000000000000000000 ) ) ;
#3032=ORIENTED_EDGE ( 'NONE', *, *, #5227, .T. ) ;
#3036=ORIENTED_EDGE ( 'NONE', *, *, #2570, .F. ) ;
#3040=FACE_OUTER_BOUND ( 'NONE', #3237, .T. ) ;
#3041=CARTESIAN_POINT ( 'NONE',  ( -3.061616997868383043E-15, -25.00000000000000000, -130.0000000000000000 ) ) ;
#3042=CARTESIAN_POINT ( 'NONE',  ( 44.00000000000000000, -13.41640786499874771, 15.00000000000000000 ) ) ;
#3045=EDGE_CURVE ( 'NONE', #5103, #5880, #6278, .T. ) ;
#3049=DIRECTION ( 'NONE',  ( -0.000000000000000000, 0.000000000000000000, -1.000000000000000000 ) ) ;
#3053=ORIENTED_EDGE ( 'NONE', *, *, #3958, .F. ) ;
#3058=ADVANCED_FACE ( 'NONE', ( #2581 ), #2070, .T. ) ;
#3060=DIRECTION ( 'NONE',  ( 1.000000000000000000, 0.000000000000000000, 0.000000000000000000 ) ) ;
#3061=VERTEX_POINT ( 'NONE', #4428 ) ;
#3062=CARTESIAN_POINT ( 'NONE',  ( -17.00000000000000000, 0.000000000000000000, 23.00000000000000000 ) ) ;
#3065=( GEOMETRIC_REPRESENTATION_CONTEXT ( 3 ) GLOBAL_UNCERTAINTY_ASSIGNED_CONTEXT ( ( #2241 ) ) GLOBAL_UNIT_ASSIGNED_CONTEXT ( ( #3940, #535, #1065 ) ) REPRESENTATION_CONTEXT ( 'NONE', 'WORKASPACE' ) );
#3066=EDGE_CURVE ( 'NONE', #5880, #1742, #4730, .T. ) ;
#3069=CIRCLE ( 'NONE', #302, 17.00000000000000000 ) ;
#3073=CYLINDRICAL_SURFACE ( 'NONE', #1989, 17.00000000000000000 ) ;
#3075=CIRCLE ( 'NONE', #4720, 19.00000000000000000 ) ;
#3077=DIRECTION ( 'NONE',  ( -0.000000000000000000, -0.000000000000000000, -1.000000000000000000 ) ) ;
#3082=AXIS2_PLACEMENT_3D ( 'NONE', #3230, #702, #2648 ) ;
#3088=VERTEX_POINT ( 'NONE', #3947 ) ;
#3089=VECTOR ( 'NONE', #3407, 1000.000000000000000 ) ;
#3093=EDGE_LOOP ( 'NONE', ( #3032, #5488 ) ) ;
#3098=DIRECTION ( 'NONE',  ( 0.000000000000000000, 0.000000000000000000, -1.000000000000000000 ) ) ;
#3099=EDGE_LOOP ( 'NONE', ( #4132, #5874 ) ) ;
#3100=ORIENTED_EDGE ( 'NONE', *, *, #3334, .T. ) ;
#3101=EDGE_LOOP ( 'NONE', ( #1868, #1152, #163, #2526 ) ) ;
#3102=DIRECTION ( 'NONE',  ( -0.000000000000000000, 0.000000000000000000, -1.000000000000000000 ) ) ;
#3103=DIRECTION ( 'NONE',  ( -1.000000000000000000, 0.000000000000000000, 0.000000000000000000 ) ) ;
#3105=CARTESIAN_POINT ( 'NONE',  ( -0.2052511266214760433, -21.25619793154163517, -95.00000000000000000 ) ) ;
#3107=ORIENTED_EDGE ( 'NONE', *, *, #3611, .F. ) ;
#3108=DIRECTION ( 'NONE',  ( 1.000000000000000000, 0.000000000000000000, 0.000000000000000000 ) ) ;
#3115=CARTESIAN_POINT ( 'NONE',  ( -17.00000000000000355, -25.00000000000000000, -160.0000000000000000 ) ) ;
#3118=CARTESIAN_POINT ( 'NONE',  ( 22.21770253897382474, 3.871672004622519037, -160.0000000000000284 ) ) ;
#3125=DIRECTION ( 'NONE',  ( -0.000000000000000000, -0.000000000000000000, 1.000000000000000000 ) ) ;
#3127=EDGE_CURVE ( 'NONE', #3088, #5213, #4625, .T. ) ;
#3128=EDGE_LOOP ( 'NONE', ( #1797, #268, #4045, #224 ) ) ;
#3129=EDGE_CURVE ( 'NONE', #5596, #2909, #1496, .T. ) ;
#3131=EDGE_CURVE ( 'NONE', #1557, #3426, #2766, .T. ) ;
#3133=DIRECTION ( 'NONE',  ( 0.000000000000000000, 0.000000000000000000, 1.000000000000000000 ) ) ;
#3134=DIRECTION ( 'NONE',  ( 0.000000000000000000, 0.000000000000000000, -1.000000000000000000 ) ) ;
#3137=VECTOR ( 'NONE', #6346, 1000.000000000000000 ) ;
#3145=VECTOR ( 'NONE', #4354, 1000.000000000000000 ) ;
#3146=AXIS2_PLACEMENT_3D ( 'NONE', #2691, #4659, #289 ) ;
#3148=DIRECTION ( 'NONE',  ( 0.000000000000000000, 0.000000000000000000, -1.000000000000000000 ) ) ;
#3159=DIRECTION ( 'NONE',  ( -0.000000000000000000, -0.000000000000000000, -1.000000000000000000 ) ) ;
#3165=CARTESIAN_POINT ( 'NONE',  ( -3.061616997868383043E-15, -25.00000000000000000, -95.00000000000000000 ) ) ;
#3174=ORIENTED_EDGE ( 'NONE', *, *, #2464, .F. ) ;
#3178=EDGE_LOOP ( 'NONE', ( #5769, #1016 ) ) ;
#3179=CIRCLE ( 'NONE', #4517, 19.00000000000000000 ) ;
#3182=DIRECTION ( 'NONE',  ( 1.000000000000000000, 0.000000000000000000, 0.000000000000000000 ) ) ;
#3186=DIRECTION ( 'NONE',  ( 1.000000000000000000, 0.000000000000000000, 0.000000000000000000 ) ) ;
#3189=CARTESIAN_POINT ( 'NONE',  ( 13.14183123006952947, -39.58265509608667543, -65.00000000000000000 ) ) ;
#3190=CLOSED_SHELL ( 'NONE', ( #2257, #4177, #6006, #3203, #600, #5358, #4414, #1907, #2505, #1599, #4676, #1403, #2812, #4405, #1161, #4083, #2625, #2951, #3735, #3728, #1410, #2597, #2180, #4146, #1714, #3414, #2315, #401, #4110, #6311, #6148, #983, #3459, #4590, #3211, #1168, #3874, #5500, #5303, #773, #1137, #5497, #5031, #2738, #4194, #670, #2968, #4063, #4866, #2270, #603, #746, #1806, #6171, #3502, #785, #387, #1926, #3545, #2103, #2309, #6180, #2267, #2404, #2778, #271, #3643, #5229, #1729, #1173, #3058, #5737, #2942, #1155 ) ) ;
#3191=AXIS2_PLACEMENT_3D ( 'NONE', #4519, #5924, #608 ) ;
#3194=ORIENTED_EDGE ( 'NONE', *, *, #3425, .F. ) ;
#3196=DIRECTION ( 'NONE',  ( 0.000000000000000000, 0.000000000000000000, -1.000000000000000000 ) ) ;
#3197=CARTESIAN_POINT ( 'NONE',  ( -44.43364355155666345, 29.42304313293565343, -65.00000000000000000 ) ) ;
#3198=DIRECTION ( 'NONE',  ( 1.000000000000000000, 0.000000000000000000, 0.000000000000000000 ) ) ;
#3200=ORIENTED_EDGE ( 'NONE', *, *, #2936, .T. ) ;
#3201=CARTESIAN_POINT ( 'NONE',  ( 16.23652742703164620, 37.28747423195200383, 15.00000000000000000 ) ) ;
#3202=ORIENTED_EDGE ( 'NONE', *, *, #3690, .T. ) ;
#3203=ADVANCED_FACE ( 'NONE', ( #5197 ), #694, .T. ) ;
#3207=FACE_OUTER_BOUND ( 'NONE', #4543, .T. ) ;
#3208=VERTEX_POINT ( 'NONE', #6037 ) ;
#3210=AXIS2_PLACEMENT_3D ( 'NONE', #2971, #6354, #5947 ) ;
#3211=ADVANCED_FACE ( 'NONE', ( #2641 ), #4148, .T. ) ;
#3213=DIRECTION ( 'NONE',  ( -1.000000000000000000, 0.000000000000000000, 0.000000000000000000 ) ) ;
#3217=ORIENTED_EDGE ( 'NONE', *, *, #5426, .T. ) ;
#3220=VERTEX_POINT ( 'NONE', #3578 ) ;
#3230=CARTESIAN_POINT ( 'NONE',  ( 0.000000000000000000, 0.000000000000000000, 23.00000000000000000 ) ) ;
#3233=DIRECTION ( 'NONE',  ( -0.000000000000000000, -0.000000000000000000, -1.000000000000000000 ) ) ;
#3234=VERTEX_POINT ( 'NONE', #4610 ) ;
#3235=CARTESIAN_POINT ( 'NONE',  ( 0.000000000000000000, 0.000000000000000000, -160.0000000000000284 ) ) ;
#3237=EDGE_LOOP ( 'NONE', ( #1969, #5048, #937, #2407 ) ) ;
#3238=EDGE_CURVE ( 'NONE', #5661, #4613, #2733, .T. ) ;
#3239=LINE ( 'NONE', #4300, #115 ) ;
#3240=ORIENTED_EDGE ( 'NONE', *, *, #2867, .T. ) ;
#3241=AXIS2_PLACEMENT_3D ( 'NONE', #1546, #3987, #4531 ) ;
#3244=CARTESIAN_POINT ( 'NONE',  ( 0.2052511266213280505, 21.25619793154159964, -240.0000000000000000 ) ) ;
#3247=CYLINDRICAL_SURFACE ( 'NONE', #5855, 17.00000000000000000 ) ;
#3249=ORIENTED_EDGE ( 'NONE', *, *, #2483, .F. ) ;
#3252=EDGE_LOOP ( 'NONE', ( #601, #3107, #4287, #4928 ) ) ;
#3258=CARTESIAN_POINT ( 'NONE',  ( 0.000000000000000000, 0.000000000000000000, -248.0000000000000000 ) ) ;
#3260=VERTEX_POINT ( 'NONE', #3383 ) ;
#3261=ORIENTED_EDGE ( 'NONE', *, *, #1253, .T. ) ;
#3267=DIRECTION ( 'NONE',  ( 0.000000000000000000, 0.000000000000000000, 1.000000000000000000 ) ) ;
#3268=AXIS2_PLACEMENT_3D ( 'NONE', #2838, #4714, #3297 ) ;
#3269=ORIENTED_EDGE ( 'NONE', *, *, #5908, .F. ) ;
#3272=CIRCLE ( 'NONE', #510, 89.87058297576894006 ) ;
#3277=EDGE_LOOP ( 'NONE', ( #5062, #1348, #6184, #1977 ) ) ;
#3281=DIRECTION ( 'NONE',  ( 1.000000000000000000, 0.000000000000000000, 0.000000000000000000 ) ) ;
#3283=ORIENTED_EDGE ( 'NONE', *, *, #5236, .F. ) ;
#3284=CARTESIAN_POINT ( 'NONE',  ( -44.00000000000000000, -13.41640786499873172, -240.0000000000000000 ) ) ;
#3289=AXIS2_PLACEMENT_3D ( 'NONE', #986, #4910, #6007 ) ;
#3292=ORIENTED_EDGE ( 'NONE', *, *, #1241, .T. ) ;
#3297=DIRECTION ( 'NONE',  ( 1.000000000000000000, 0.000000000000000000, 0.000000000000000000 ) ) ;
#3299=EDGE_LOOP ( 'NONE', ( #1451, #2661, #3677, #71 ) ) ;
#3301=VECTOR ( 'NONE', #5710, 1000.000000000000000 ) ;
#3304=CARTESIAN_POINT ( 'NONE',  ( 17.00000000000000000, 25.00000000000000355, -195.0000000000000000 ) ) ;
#3305=ORIENTED_EDGE ( 'NONE', *, *, #588, .T. ) ;
#3307=VERTEX_POINT ( 'NONE', #1487 ) ;
#3315=DIRECTION ( 'NONE',  ( -0.000000000000000000, -0.000000000000000000, 1.000000000000000000 ) ) ;
#3316=FACE_OUTER_BOUND ( 'NONE', #1380, .T. ) ;
#3319=EDGE_LOOP ( 'NONE', ( #3461, #904, #3495, #13 ) ) ;
#3324=EDGE_CURVE ( 'NONE', #5434, #5103, #1958, .T. ) ;
#3326=ORIENTED_EDGE ( 'NONE', *, *, #299, .T. ) ;
#3327=ORIENTED_EDGE ( 'NONE', *, *, #2577, .F. ) ;
#3334=EDGE_CURVE ( 'NONE', #2995, #602, #4100, .T. ) ;
#3335=CYLINDRICAL_SURFACE ( 'NONE', #4166, 19.00000000000000000 ) ;
#3337=DIRECTION ( 'NONE',  ( 0.000000000000000000, -0.000000000000000000, 1.000000000000000000 ) ) ;
#3338=EDGE_CURVE ( 'NONE', #5491, #1339, #1747, .T. ) ;
#3339=CARTESIAN_POINT ( 'NONE',  ( -44.00000000000000000, -13.41640786499873172, 0.000000000000000000 ) ) ;
#3340=CARTESIAN_POINT ( 'NONE',  ( 0.2052511266213299934, 21.25619793154162807, -180.0000000000000000 ) ) ;
#3343=EDGE_CURVE ( 'NONE', #3894, #4348, #5971, .T. ) ;
#3344=LINE ( 'NONE', #1004, #3137 ) ;
#3356=ORIENTED_EDGE ( 'NONE', *, *, #4671, .T. ) ;
#3359=ORIENTED_EDGE ( 'NONE', *, *, #2982, .F. ) ;
#3363=PLANE ( 'NONE',  #3379 ) ;
#3367=VERTEX_POINT ( 'NONE', #5879 ) ;
#3368=MECHANICAL_DESIGN_GEOMETRIC_PRESENTATION_REPRESENTATION('',(#1210),#3065);
#3374=CARTESIAN_POINT ( 'NONE',  ( 44.64065620456912598, 28.99954194078667413, -110.0000000000000000 ) ) ;
#3375=AXIS2_PLACEMENT_3D ( 'NONE', #3410, #5, #2479 ) ;
#3376=CARTESIAN_POINT ( 'NONE',  ( 44.00000000000009948, 13.41640786499835514, -110.0000000000000000 ) ) ;
#3377=ORIENTED_EDGE ( 'NONE', *, *, #2653, .F. ) ;
#3378=DIRECTION ( 'NONE',  ( 1.000000000000000000, 0.000000000000000000, 0.000000000000000000 ) ) ;
#3379=AXIS2_PLACEMENT_3D ( 'NONE', #2882, #4853, #1921 ) ;
#3383=CARTESIAN_POINT ( 'NONE',  ( 13.14183123006952947, -39.58265509608667543, -160.0000000000000284 ) ) ;
#3384=ORIENTED_EDGE ( 'NONE', *, *, #1892, .F. ) ;
#3385=CIRCLE ( 'NONE', #4199, 89.87058297576892585 ) ;
#3386=CARTESIAN_POINT ( 'NONE',  ( -44.43364355155666345, 29.42304313293564988, -110.0000000000000000 ) ) ;
#3389=CIRCLE ( 'NONE', #727, 46.00000000000000000 ) ;
#3392=DIRECTION ( 'NONE',  ( -1.000000000000000000, 0.000000000000000000, 0.000000000000000000 ) ) ;
#3393=EDGE_CURVE ( 'NONE', #6099, #3894, #3389, .T. ) ;
#3399=AXIS2_PLACEMENT_3D ( 'NONE', #688, #5098, #5127 ) ;
#3402=ORIENTED_EDGE ( 'NONE', *, *, #5427, .F. ) ;
#3407=DIRECTION ( 'NONE',  ( -0.000000000000000000, -0.000000000000000000, 1.000000000000000000 ) ) ;
#3410=CARTESIAN_POINT ( 'NONE',  ( -44.64065620456893413, -28.99954194078699032, -195.0000000000000000 ) ) ;
#3411=EDGE_CURVE ( 'NONE', #4956, #4783, #42, .T. ) ;
#3414=ADVANCED_FACE ( 'NONE', ( #5999, #1573 ), #5942, .T. ) ;
#3418=EDGE_LOOP ( 'NONE', ( #5921, #2704, #2717, #2642 ) ) ;
#3419=ORIENTED_EDGE ( 'NONE', *, *, #313, .T. ) ;
#3421=CARTESIAN_POINT ( 'NONE',  ( 19.00000000000000000, 2.326828918379970970E-15, 23.00000000000000000 ) ) ;
#3422=DIRECTION ( 'NONE',  ( -0.000000000000000000, 0.000000000000000000, -1.000000000000000000 ) ) ;
#3423=CYLINDRICAL_SURFACE ( 'NONE', #4934, 89.87058297576894006 ) ;
#3425=EDGE_CURVE ( 'NONE', #6099, #1071, #458, .T. ) ;
#3426=VERTEX_POINT ( 'NONE', #3633 ) ;
#3428=ORIENTED_EDGE ( 'NONE', *, *, #2763, .T. ) ;
#3430=DIRECTION ( 'NONE',  ( -0.000000000000000000, -0.000000000000000000, 1.000000000000000000 ) ) ;
#3431=FACE_BOUND ( 'NONE', #2326, .T. ) ;
#3436=DIRECTION ( 'NONE',  ( -0.000000000000000000, -0.000000000000000000, -1.000000000000000000 ) ) ;
#3439=CARTESIAN_POINT ( 'NONE',  ( 0.2052511266213280505, 21.25619793154159964, 15.00000000000000000 ) ) ;
#3441=DIRECTION ( 'NONE',  ( -0.000000000000000000, -0.000000000000000000, -1.000000000000000000 ) ) ;
#3444=EDGE_CURVE ( 'NONE', #1742, #4844, #5641, .T. ) ;
#3445=CARTESIAN_POINT ( 'NONE',  ( 13.14183123006952947, -39.58265509608667543, -160.0000000000000284 ) ) ;
#3449=EDGE_CURVE ( 'NONE', #5709, #2780, #4209, .T. ) ;
#3457=LINE ( 'NONE', #2519, #2981 ) ;
#3459=ADVANCED_FACE ( 'NONE', ( #2606 ), #1183, .T. ) ;
#3461=ORIENTED_EDGE ( 'NONE', *, *, #4671, .F. ) ;
#3462=CIRCLE ( 'NONE', #1603, 19.00000000000000000 ) ;
#3463=CIRCLE ( 'NONE', #691, 17.00000000000000000 ) ;
#3466=CARTESIAN_POINT ( 'NONE',  ( -43.99999999999987921, 13.41640786499904969, -110.0000000000000000 ) ) ;
#3467=EDGE_CURVE ( 'NONE', #453, #3504, #3179, .T. ) ;
#3469=DIRECTION ( 'NONE',  ( 0.000000000000000000, 0.000000000000000000, 1.000000000000000000 ) ) ;
#3471=AXIS2_PLACEMENT_3D ( 'NONE', #3873, #5791, #1366 ) ;
#3474=DIRECTION ( 'NONE',  ( -0.000000000000000000, -0.000000000000000000, -1.000000000000000000 ) ) ;
#3475=EDGE_LOOP ( 'NONE', ( #1889, #5933, #1024, #2101 ) ) ;
#3477=DIRECTION ( 'NONE',  ( 1.000000000000000000, 0.000000000000000000, 0.000000000000000000 ) ) ;
#3478=AXIS2_PLACEMENT_3D ( 'NONE', #5740, #1312, #5702 ) ;
#3479=DIRECTION ( 'NONE',  ( -0.000000000000000000, 0.000000000000000000, -1.000000000000000000 ) ) ;
#3482=LINE ( 'NONE', #1904, #72 ) ;
#3486=VECTOR ( 'NONE', #3031, 1000.000000000000000 ) ;
#3489=PLANE ( 'NONE',  #3001 ) ;
#3490=CIRCLE ( 'NONE', #1112, 22.67164836619066648 ) ;
#3492=AXIS2_PLACEMENT_3D ( 'NONE', #2017, #1502, #3978 ) ;
#3493=DIRECTION ( 'NONE',  ( -0.000000000000000000, -0.000000000000000000, -1.000000000000000000 ) ) ;
#3495=ORIENTED_EDGE ( 'NONE', *, *, #4286, .T. ) ;
#3496=AXIS2_PLACEMENT_3D ( 'NONE', #3521, #5036, #1093 ) ;
#3502=ADVANCED_FACE ( 'NONE', ( #4534, #2092 ), #6091, .F. ) ;
#3503=CARTESIAN_POINT ( 'NONE',  ( 0.000000000000000000, 0.000000000000000000, 23.00000000000000000 ) ) ;
#3504=VERTEX_POINT ( 'NONE', #4044 ) ;
#3505=AXIS2_PLACEMENT_3D ( 'NONE', #5190, #779, #4699 ) ;
#3513=AXIS2_PLACEMENT_3D ( 'NONE', #5290, #4732, #6187 ) ;
#3515=EDGE_LOOP ( 'NONE', ( #3885, #3359 ) ) ;
#3516=DIRECTION ( 'NONE',  ( 1.000000000000000000, 0.000000000000000000, 0.000000000000000000 ) ) ;
#3517=CARTESIAN_POINT ( 'NONE',  ( 44.64065620456912598, 28.99954194078667413, -175.0000000000000284 ) ) ;
#3521=CARTESIAN_POINT ( 'NONE',  ( -0.2052511266214760433, -21.25619793154163517, -115.0000000000000000 ) ) ;
#3523=ORIENTED_EDGE ( 'NONE', *, *, #595, .F. ) ;
#3524=ORIENTED_EDGE ( 'NONE', *, *, #5147, .T. ) ;
#3528=CARTESIAN_POINT ( 'NONE',  ( 44.00000000000000000, -13.41640786499874771, -225.0000000000000000 ) ) ;
#3533=EDGE_CURVE ( 'NONE', #4515, #3234, #1646, .T. ) ;
#3535=CARTESIAN_POINT ( 'NONE',  ( -17.00000000000000000, 0.000000000000000000, -180.0000000000000000 ) ) ;
#3543=CARTESIAN_POINT ( 'NONE',  ( -22.21770253897380343, -3.871672004622680241, -30.00000000000000000 ) ) ;
#3544=EDGE_LOOP ( 'NONE', ( #5599, #3998, #3841, #4578 ) ) ;
#3545=ADVANCED_FACE ( 'NONE', ( #6253 ), #4339, .T. ) ;
#3546=CYLINDRICAL_SURFACE ( 'NONE', #1730, 17.00000000000000000 ) ;
#3554=VERTEX_POINT ( 'NONE', #6318 ) ;
#3559=CARTESIAN_POINT ( 'NONE',  ( 0.000000000000000000, 0.000000000000000000, 48.00000000000000000 ) ) ;
#3564=VECTOR ( 'NONE', #1252, 1000.000000000000000 ) ;
#3568=DIRECTION ( 'NONE',  ( -0.000000000000000000, -0.000000000000000000, -1.000000000000000000 ) ) ;
#3569=CARTESIAN_POINT ( 'NONE',  ( 44.00000000000000000, -13.41640786499873705, -180.0000000000000000 ) ) ;
#3570=AXIS2_PLACEMENT_3D ( 'NONE', #5751, #2829, #1324 ) ;
#3578=CARTESIAN_POINT ( 'NONE',  ( 44.00000000000000000, -13.41640786499873705, -195.0000000000000000 ) ) ;
#3587=CARTESIAN_POINT ( 'NONE',  ( 13.14183123006966980, -39.58265509608656174, -115.0000000000000000 ) ) ;
#3589=AXIS2_PLACEMENT_3D ( 'NONE', #4716, #3134, #3198 ) ;
#3591=ORIENTED_EDGE ( 'NONE', *, *, #5930, .T. ) ;
#3598=AXIS2_PLACEMENT_3D ( 'NONE', #3439, #5413, #4927 ) ;
#3600=FACE_OUTER_BOUND ( 'NONE', #3782, .T. ) ;
#3601=EDGE_CURVE ( 'NONE', #3061, #2498, #4521, .T. ) ;
#3611=EDGE_CURVE ( 'NONE', #1995, #2333, #62, .T. ) ;
#3612=AXIS2_PLACEMENT_3D ( 'NONE', #1770, #4661, #254 ) ;
#3614=DIRECTION ( 'NONE',  ( -0.000000000000000000, -0.000000000000000000, 1.000000000000000000 ) ) ;
#3619=EDGE_CURVE ( 'NONE', #161, #2613, #1001, .T. ) ;
#3623=ORIENTED_EDGE ( 'NONE', *, *, #3444, .F. ) ;
#3628=VERTEX_POINT ( 'NONE', #5835 ) ;
#3633=CARTESIAN_POINT ( 'NONE',  ( 17.00000000000000000, 0.000000000000000000, -248.0000000000000000 ) ) ;
#3634=ORIENTED_EDGE ( 'NONE', *, *, #5236, .T. ) ;
#3643=ADVANCED_FACE ( 'NONE', ( #5476 ), #3859, .T. ) ;
#3645=ORIENTED_EDGE ( 'NONE', *, *, #2082, .T. ) ;
#3646=LINE ( 'NONE', #606, #1503 ) ;
#3650=CARTESIAN_POINT ( 'NONE',  ( 0.000000000000000000, 0.000000000000000000, -175.0000000000000284 ) ) ;
#3653=DIRECTION ( 'NONE',  ( -1.000000000000000000, 0.000000000000000000, 0.000000000000000000 ) ) ;
#3656=CARTESIAN_POINT ( 'NONE',  ( -44.00000000000000000, -13.41640786499873172, 15.00000000000000000 ) ) ;
#3672=CIRCLE ( 'NONE', #4180, 17.00000000000000000 ) ;
#3677=ORIENTED_EDGE ( 'NONE', *, *, #313, .F. ) ;
#3683=FACE_BOUND ( 'NONE', #4449, .T. ) ;
#3684=EDGE_LOOP ( 'NONE', ( #3727, #2495 ) ) ;
#3690=EDGE_CURVE ( 'NONE', #1488, #5709, #4946, .T. ) ;
#3693=AXIS2_PLACEMENT_3D ( 'NONE', #6359, #2332, #4482 ) ;
#3695=AXIS2_PLACEMENT_3D ( 'NONE', #1534, #3430, #1585 ) ;
#3698=ORIENTED_EDGE ( 'NONE', *, *, #2591, .T. ) ;
#3703=LINE ( 'NONE', #6252, #3564 ) ;
#3718=ORIENTED_EDGE ( 'NONE', *, *, #5161, .T. ) ;
#3719=DIRECTION ( 'NONE',  ( -0.000000000000000000, -0.000000000000000000, -1.000000000000000000 ) ) ;
#3727=ORIENTED_EDGE ( 'NONE', *, *, #1148, .F. ) ;
#3728=ADVANCED_FACE ( 'NONE', ( #970 ), #2509, .T. ) ;
#3729=DIRECTION ( 'NONE',  ( 0.000000000000000000, 0.000000000000000000, 1.000000000000000000 ) ) ;
#3733=CARTESIAN_POINT ( 'NONE',  ( 16.99999999999999645, -25.00000000000000000, -95.00000000000000000 ) ) ;
#3734=EDGE_LOOP ( 'NONE', ( #4755, #1424, #4411, #5471 ) ) ;
#3735=ADVANCED_FACE ( 'NONE', ( #5900 ), #4985, .T. ) ;
#3741=DIRECTION ( 'NONE',  ( 0.000000000000000000, 0.000000000000000000, -1.000000000000000000 ) ) ;
#3744=ORIENTED_EDGE ( 'NONE', *, *, #4153, .F. ) ;
#3747=LINE ( 'NONE', #5711, #1501 ) ;
#3748=EDGE_CURVE ( 'NONE', #43, #1691, #3813, .T. ) ;
#3752=EDGE_LOOP ( 'NONE', ( #3821, #2005, #911, #4150 ) ) ;
#3756=DIRECTION ( 'NONE',  ( 1.000000000000000000, 0.000000000000000000, 0.000000000000000000 ) ) ;
#3759=ORIENTED_EDGE ( 'NONE', *, *, #5614, .T. ) ;
#3762=CARTESIAN_POINT ( 'NONE',  ( -13.14183123006980480, 39.58265509608657595, -180.0000000000000000 ) ) ;
#3763=ORIENTED_EDGE ( 'NONE', *, *, #1246, .F. ) ;
#3766=AXIS2_PLACEMENT_3D ( 'NONE', #301, #2252, #4221 ) ;
#3768=AXIS2_PLACEMENT_3D ( 'NONE', #5898, #3337, #4858 ) ;
#3779=FACE_BOUND ( 'NONE', #179, .T. ) ;
#3781=ORIENTED_EDGE ( 'NONE', *, *, #2721, .T. ) ;
#3782=EDGE_LOOP ( 'NONE', ( #5191, #4977 ) ) ;
#3785=CYLINDRICAL_SURFACE ( 'NONE', #2639, 90.00000000000319744 ) ;
#3789=ORIENTED_EDGE ( 'NONE', *, *, #1452, .T. ) ;
#3793=ORIENTED_EDGE ( 'NONE', *, *, #3045, .F. ) ;
#3794=DIRECTION ( 'NONE',  ( -0.000000000000000000, -0.000000000000000000, 1.000000000000000000 ) ) ;
#3795=ORIENTED_EDGE ( 'NONE', *, *, #5837, .F. ) ;
#3799=DIRECTION ( 'NONE',  ( 0.000000000000000000, 0.000000000000000000, -1.000000000000000000 ) ) ;
#3803=AXIS2_PLACEMENT_3D ( 'NONE', #79, #1469, #3972 ) ;
#3805=DIRECTION ( 'NONE',  ( 1.000000000000000000, 0.000000000000000000, 0.000000000000000000 ) ) ;
#3807=AXIS2_PLACEMENT_3D ( 'NONE', #2153, #1119, #3060 ) ;
#3813=CIRCLE ( 'NONE', #4836, 17.00000000000000000 ) ;
#3815=AXIS2_PLACEMENT_3D ( 'NONE', #3235, #1688, #2713 ) ;
#3818=CARTESIAN_POINT ( 'NONE',  ( 0.000000000000000000, 0.000000000000000000, -273.0000000000000000 ) ) ;
#3821=ORIENTED_EDGE ( 'NONE', *, *, #1922, .T. ) ;
#3832=FACE_BOUND ( 'NONE', #2223, .T. ) ;
#3836=DIRECTION ( 'NONE',  ( -0.000000000000000000, -0.000000000000000000, 1.000000000000000000 ) ) ;
#3841=ORIENTED_EDGE ( 'NONE', *, *, #2000, .T. ) ;
#3853=DIRECTION ( 'NONE',  ( 1.000000000000000000, 0.000000000000000000, -0.000000000000000000 ) ) ;
#3855=CARTESIAN_POINT ( 'NONE',  ( 0.000000000000000000, 0.000000000000000000, 23.00000000000000000 ) ) ;
#3859=CYLINDRICAL_SURFACE ( 'NONE', #2989, 89.99999999999998579 ) ;
#3863=LINE ( 'NONE', #5325, #5412 ) ;
#3865=DIRECTION ( 'NONE',  ( -0.000000000000000000, -0.000000000000000000, -1.000000000000000000 ) ) ;
#3871=DIRECTION ( 'NONE',  ( 0.000000000000000000, -0.000000000000000000, 1.000000000000000000 ) ) ;
#3873=CARTESIAN_POINT ( 'NONE',  ( 0.000000000000000000, 25.00000000000000000, -225.0000000000000000 ) ) ;
#3874=ADVANCED_FACE ( 'NONE', ( #2146 ), #2088, .T. ) ;
#3875=DIRECTION ( 'NONE',  ( -0.000000000000000000, -0.000000000000000000, -1.000000000000000000 ) ) ;
#3876=ORIENTED_EDGE ( 'NONE', *, *, #3994, .F. ) ;
#3878=CARTESIAN_POINT ( 'NONE',  ( -17.00000000000000000, 2.081899558550500280E-15, -115.0000000000000000 ) ) ;
#3885=ORIENTED_EDGE ( 'NONE', *, *, #938, .F. ) ;
#3887=AXIS2_PLACEMENT_3D ( 'NONE', #683, #4599, #201 ) ;
#3888=CYLINDRICAL_SURFACE ( 'NONE', #175, 17.00000000000000000 ) ;
#3889=EDGE_CURVE ( 'NONE', #1881, #6115, #2115, .T. ) ;
#3891=CYLINDRICAL_SURFACE ( 'NONE', #4791, 46.00000000000000000 ) ;
#3894=VERTEX_POINT ( 'NONE', #743 ) ;
#3899=CARTESIAN_POINT ( 'NONE',  ( -44.43364355155666345, 29.42304313293564988, -130.0000000000000000 ) ) ;
#3901=DIRECTION ( 'NONE',  ( 1.000000000000000000, 0.000000000000000000, 0.000000000000000000 ) ) ;
#3905=CARTESIAN_POINT ( 'NONE',  ( 16.23652742703164620, 37.28747423195200383, -225.0000000000000000 ) ) ;
#3909=DIRECTION ( 'NONE',  ( -0.000000000000000000, -0.000000000000000000, 1.000000000000000000 ) ) ;
#3910=FACE_OUTER_BOUND ( 'NONE', #4788, .T. ) ;
#3914=ORIENTED_EDGE ( 'NONE', *, *, #2763, .F. ) ;
#3915=ORIENTED_EDGE ( 'NONE', *, *, #2393, .T. ) ;
#3920=CARTESIAN_POINT ( 'NONE',  ( 13.14183123006966980, -39.58265509608656174, -95.00000000000000000 ) ) ;
#3925=EDGE_CURVE ( 'NONE', #3208, #4113, #2207, .T. ) ;
#3927=PLANE ( 'NONE',  #587 ) ;
#3932=ORIENTED_EDGE ( 'NONE', *, *, #5706, .F. ) ;
#3933=EDGE_CURVE ( 'NONE', #4645, #2995, #5258, .T. ) ;
#3934=CYLINDRICAL_SURFACE ( 'NONE', #4191, 19.00000000000000000 ) ;
#3935=DIRECTION ( 'NONE',  ( -0.000000000000000000, -0.000000000000000000, -1.000000000000000000 ) ) ;
#3938=DIRECTION ( 'NONE',  ( -0.000000000000000000, -0.000000000000000000, -1.000000000000000000 ) ) ;
#3940=( LENGTH_UNIT ( ) NAMED_UNIT ( * ) SI_UNIT ( .MILLI., .METRE. ) );
#3942=DIRECTION ( 'NONE',  ( -1.000000000000000000, 0.000000000000000000, 0.000000000000000000 ) ) ;
#3944=DIRECTION ( 'NONE',  ( -0.000000000000000000, -0.000000000000000000, 1.000000000000000000 ) ) ;
#3945=AXIS2_PLACEMENT_3D ( 'NONE', #2218, #4179, #2803 ) ;
#3947=CARTESIAN_POINT ( 'NONE',  ( -16.23652742703190199, -37.28747423195189015, -65.00000000000000000 ) ) ;
#3950=ORIENTED_EDGE ( 'NONE', *, *, #3129, .F. ) ;
#3953=DIRECTION ( 'NONE',  ( 1.000000000000000000, 0.000000000000000000, 0.000000000000000000 ) ) ;
#3955=VERTEX_POINT ( 'NONE', #4787 ) ;
#3958=EDGE_CURVE ( 'NONE', #453, #2206, #5311, .T. ) ;
#3960=ORIENTED_EDGE ( 'NONE', *, *, #1253, .F. ) ;
#3962=FACE_OUTER_BOUND ( 'NONE', #4725, .T. ) ;
#3964=DIRECTION ( 'NONE',  ( -1.000000000000000000, 0.000000000000000000, 0.000000000000000000 ) ) ;
#3970=PLANE ( 'NONE',  #5993 ) ;
#3972=DIRECTION ( 'NONE',  ( -1.000000000000000000, 0.000000000000000000, 0.000000000000000000 ) ) ;
#3974=EDGE_LOOP ( 'NONE', ( #2759, #3960, #1643, #614 ) ) ;
#3975=AXIS2_PLACEMENT_3D ( 'NONE', #4951, #546, #1561 ) ;
#3978=DIRECTION ( 'NONE',  ( -1.000000000000000000, 0.000000000000000000, 0.000000000000000000 ) ) ;
#3984=ORIENTED_EDGE ( 'NONE', *, *, #1058, .T. ) ;
#3987=DIRECTION ( 'NONE',  ( -0.000000000000000000, -0.000000000000000000, 1.000000000000000000 ) ) ;
#3989=CARTESIAN_POINT ( 'NONE',  ( -44.00000000000000000, -13.41640786499873350, -45.00000000000000000 ) ) ;
#3994=EDGE_CURVE ( 'NONE', #4815, #4122, #3239, .T. ) ;
#3995=CARTESIAN_POINT ( 'NONE',  ( 0.000000000000000000, 0.000000000000000000, -110.0000000000000000 ) ) ;
#3996=AXIS2_PLACEMENT_3D ( 'NONE', #3165, #5077, #4190 ) ;
#3998=ORIENTED_EDGE ( 'NONE', *, *, #5716, .T. ) ;
#3999=ORIENTED_EDGE ( 'NONE', *, *, #1330, .F. ) ;
#4006=DIRECTION ( 'NONE',  ( 0.000000000000000000, 0.000000000000000000, 1.000000000000000000 ) ) ;
#4011=EDGE_CURVE ( 'NONE', #3367, #3955, #2845, .T. ) ;
#4012=DIRECTION ( 'NONE',  ( -0.000000000000000000, 0.000000000000000000, -1.000000000000000000 ) ) ;
#4021=AXIS2_PLACEMENT_3D ( 'NONE', #5218, #5739, #1214 ) ;
#4022=DIRECTION ( 'NONE',  ( -0.000000000000000000, -0.000000000000000000, 1.000000000000000000 ) ) ;
#4027=DIRECTION ( 'NONE',  ( 1.000000000000000000, 0.000000000000000000, 0.000000000000000000 ) ) ;
#4030=ORIENTED_EDGE ( 'NONE', *, *, #1326, .F. ) ;
#4032=FACE_OUTER_BOUND ( 'NONE', #5293, .T. ) ;
#4033=LINE ( 'NONE', #1100, #2865 ) ;
#4035=CARTESIAN_POINT ( 'NONE',  ( 0.000000000000000000, 0.000000000000000000, -248.0000000000000000 ) ) ;
#4036=ORIENTED_EDGE ( 'NONE', *, *, #4833, .T. ) ;
#4044=CARTESIAN_POINT ( 'NONE',  ( 19.00000000000000000, 0.000000000000000000, -248.0000000000000000 ) ) ;
#4045=ORIENTED_EDGE ( 'NONE', *, *, #6217, .F. ) ;
#4050=CARTESIAN_POINT ( 'NONE',  ( 0.000000000000000000, 0.000000000000000000, -175.0000000000000000 ) ) ;
#4057=DIRECTION ( 'NONE',  ( -0.000000000000000000, -0.000000000000000000, -1.000000000000000000 ) ) ;
#4058=EDGE_CURVE ( 'NONE', #5299, #2249, #2371, .T. ) ;
#4061=FACE_OUTER_BOUND ( 'NONE', #5829, .T. ) ;
#4062=EDGE_LOOP ( 'NONE', ( #1558, #2427, #729, #5814 ) ) ;
#4063=ADVANCED_FACE ( 'NONE', ( #3207 ), #286, .T. ) ;
#4069=ORIENTED_EDGE ( 'NONE', *, *, #5716, .F. ) ;
#4071=ORIENTED_EDGE ( 'NONE', *, *, #5533, .F. ) ;
#4079=EDGE_LOOP ( 'NONE', ( #2644, #2496, #4197, #269 ) ) ;
#4083=ADVANCED_FACE ( 'NONE', ( #4919, #3431 ), #518, .T. ) ;
#4087=EDGE_LOOP ( 'NONE', ( #5000, #4431, #813, #2950 ) ) ;
#4090=VECTOR ( 'NONE', #2338, 1000.000000000000000 ) ;
#4093=DIRECTION ( 'NONE',  ( 1.000000000000000000, 0.000000000000000000, 0.000000000000000000 ) ) ;
#4094=CARTESIAN_POINT ( 'NONE',  ( 44.00000000000000000, -13.41640786499874771, -240.0000000000000000 ) ) ;
#4100=CIRCLE ( 'NONE', #528, 90.00000000000000000 ) ;
#4107=EDGE_LOOP ( 'NONE', ( #3053, #1434, #2770, #711 ) ) ;
#4108=CYLINDRICAL_SURFACE ( 'NONE', #1695, 90.00000000000321165 ) ;
#4109=DIRECTION ( 'NONE',  ( 1.000000000000000000, 0.000000000000000000, -0.000000000000000000 ) ) ;
#4110=ADVANCED_FACE ( 'NONE', ( #4061 ), #573, .T. ) ;
#4113=VERTEX_POINT ( 'NONE', #6048 ) ;
#4114=CIRCLE ( 'NONE', #5053, 17.00000000000000000 ) ;
#4117=CIRCLE ( 'NONE', #3513, 90.00000000000319744 ) ;
#4122=VERTEX_POINT ( 'NONE', #4128 ) ;
#4123=DIRECTION ( 'NONE',  ( 0.000000000000000000, 0.000000000000000000, -1.000000000000000000 ) ) ;
#4124=EDGE_CURVE ( 'NONE', #1758, #6160, #406, .T. ) ;
#4125=CARTESIAN_POINT ( 'NONE',  ( -2.385244779468109755E-15, -1.040834085586084257E-14, -110.0000000000000000 ) ) ;
#4127=DIRECTION ( 'NONE',  ( -0.000000000000000000, -0.000000000000000000, 1.000000000000000000 ) ) ;
#4128=CARTESIAN_POINT ( 'NONE',  ( 17.00000000000000000, 25.00000000000000355, -225.0000000000000000 ) ) ;
#4129=ORIENTED_EDGE ( 'NONE', *, *, #3601, .F. ) ;
#4131=AXIS2_PLACEMENT_3D ( 'NONE', #5332, #1947, #982 ) ;
#4132=ORIENTED_EDGE ( 'NONE', *, *, #5426, .F. ) ;
#4141=CARTESIAN_POINT ( 'NONE',  ( 19.00000000000000000, 2.326828918379970970E-15, 15.00000000000000000 ) ) ;
#4143=CARTESIAN_POINT ( 'NONE',  ( 0.000000000000000000, 0.000000000000000000, -273.0000000000000000 ) ) ;
#4146=ADVANCED_FACE ( 'NONE', ( #1103 ), #2137, .T. ) ;
#4148=CYLINDRICAL_SURFACE ( 'NONE', #5876, 89.87058297576892585 ) ;
#4149=ORIENTED_EDGE ( 'NONE', *, *, #5024, .F. ) ;
#4150=ORIENTED_EDGE ( 'NONE', *, *, #3425, .T. ) ;
#4151=CARTESIAN_POINT ( 'NONE',  ( -15.82602517378898987, 37.28747423195201094, 15.00000000000000000 ) ) ;
#4153=EDGE_CURVE ( 'NONE', #1758, #738, #5495, .T. ) ;
#4155=DIRECTION ( 'NONE',  ( 1.000000000000000000, 0.000000000000000000, 0.000000000000000000 ) ) ;
#4156=FACE_OUTER_BOUND ( 'NONE', #5489, .T. ) ;
#4157=ORIENTED_EDGE ( 'NONE', *, *, #5812, .F. ) ;
#4158=PLANE ( 'NONE',  #1719 ) ;
#4163=DIRECTION ( 'NONE',  ( -0.000000000000000000, -0.000000000000000000, 1.000000000000000000 ) ) ;
#4166=AXIS2_PLACEMENT_3D ( 'NONE', #3855, #2850, #1478 ) ;
#4168=UNCERTAINTY_MEASURE_WITH_UNIT (LENGTH_MEASURE( 1.000000000000000082E-05 ), #1280, 'distance_accuracy_value', 'NONE');
#4169=DIRECTION ( 'NONE',  ( 1.000000000000000000, 0.000000000000000000, 0.000000000000000000 ) ) ;
#4170=CARTESIAN_POINT ( 'NONE',  ( 0.000000000000000000, 0.000000000000000000, -115.0000000000000000 ) ) ;
#4173=ORIENTED_EDGE ( 'NONE', *, *, #6105, .F. ) ;
#4177=ADVANCED_FACE ( 'NONE', ( #1660 ), #4622, .T. ) ;
#4179=DIRECTION ( 'NONE',  ( 0.000000000000000000, 0.000000000000000000, -1.000000000000000000 ) ) ;
#4180=AXIS2_PLACEMENT_3D ( 'NONE', #4848, #312, #858 ) ;
#4181=EDGE_CURVE ( 'NONE', #4348, #4113, #3272, .T. ) ;
#4184=EDGE_CURVE ( 'NONE', #161, #5556, #5337, .T. ) ;
#4185=ORIENTED_EDGE ( 'NONE', *, *, #108, .F. ) ;
#4190=DIRECTION ( 'NONE',  ( -1.000000000000000000, 0.000000000000000000, 0.000000000000000000 ) ) ;
#4191=AXIS2_PLACEMENT_3D ( 'NONE', #5450, #3441, #1031 ) ;
#4194=ADVANCED_FACE ( 'NONE', ( #613 ), #2049, .T. ) ;
#4197=ORIENTED_EDGE ( 'NONE', *, *, #3066, .T. ) ;
#4199=AXIS2_PLACEMENT_3D ( 'NONE', #3197, #5203, #4093 ) ;
#4200=CARTESIAN_POINT ( 'NONE',  ( 44.56092774862622719, -29.44644455561813956, 15.00000000000000000 ) ) ;
#4204=CIRCLE ( 'NONE', #5653, 17.00000000000000000 ) ;
#4209=CIRCLE ( 'NONE', #215, 22.67164836619068424 ) ;
#4211=EDGE_CURVE ( 'NONE', #4844, #760, #1313, .T. ) ;
#4213=CARTESIAN_POINT ( 'NONE',  ( 17.00000000000000000, 0.000000000000000000, -45.00000000000000000 ) ) ;
#4215=VECTOR ( 'NONE', #2056, 1000.000000000000000 ) ;
#4217=ORIENTED_EDGE ( 'NONE', *, *, #4268, .F. ) ;
#4218=CYLINDRICAL_SURFACE ( 'NONE', #1321, 46.00000000000000000 ) ;
#4221=DIRECTION ( 'NONE',  ( -1.000000000000000000, 0.000000000000000000, 0.000000000000000000 ) ) ;
#4223=CIRCLE ( 'NONE', #3399, 17.00000000000000000 ) ;
#4226=ORIENTED_EDGE ( 'NONE', *, *, #2393, .F. ) ;
#4227=ORIENTED_EDGE ( 'NONE', *, *, #5078, .T. ) ;
#4235=DIRECTION ( 'NONE',  ( -0.000000000000000000, -0.000000000000000000, -1.000000000000000000 ) ) ;
#4238=ORIENTED_EDGE ( 'NONE', *, *, #1241, .F. ) ;
#4242=FACE_OUTER_BOUND ( 'NONE', #4797, .T. ) ;
#4246=ORIENTED_EDGE ( 'NONE', *, *, #4756, .F. ) ;
#4254=PRODUCT_DEFINITION_FORMATION_WITH_SPECIFIED_SOURCE ( 'ANY', '', #2145, .NOT_KNOWN. ) ;
#4257=DIRECTION ( 'NONE',  ( 1.000000000000000000, 0.000000000000000000, 0.000000000000000000 ) ) ;
#4258=ORIENTED_EDGE ( 'NONE', *, *, #5706, .T. ) ;
#4260=FACE_OUTER_BOUND ( 'NONE', #2138, .T. ) ;
#4268=EDGE_CURVE ( 'NONE', #1077, #5299, #1272, .T. ) ;
#4269=LINE ( 'NONE', #6248, #1401 ) ;
#4272=DIRECTION ( 'NONE',  ( -1.000000000000000000, 0.000000000000000000, 0.000000000000000000 ) ) ;
#4276=AXIS2_PLACEMENT_3D ( 'NONE', #917, #6235, #344 ) ;
#4278=CARTESIAN_POINT ( 'NONE',  ( -43.99999999999990052, 13.41640786499905147, -175.0000000000000284 ) ) ;
#4280=CARTESIAN_POINT ( 'NONE',  ( 44.00000000000000000, -13.41640786499873705, -180.0000000000000000 ) ) ;
#4284=VERTEX_POINT ( 'NONE', #460 ) ;
#4286=EDGE_CURVE ( 'NONE', #5613, #6010, #4297, .T. ) ;
#4287=ORIENTED_EDGE ( 'NONE', *, *, #327, .F. ) ;
#4289=VECTOR ( 'NONE', #2518, 1000.000000000000000 ) ;
#4290=CARTESIAN_POINT ( 'NONE',  ( 44.00000000000008527, 13.41640786499836224, -65.00000000000000000 ) ) ;
#4291=CYLINDRICAL_SURFACE ( 'NONE', #4401, 17.00000000000000000 ) ;
#4292=CARTESIAN_POINT ( 'NONE',  ( -44.64065620456596406, -28.99954194078535963, 0.000000000000000000 ) ) ;
#4293=AXIS2_PLACEMENT_3D ( 'NONE', #778, #5670, #4272 ) ;
#4297=CIRCLE ( 'NONE', #913, 90.00000000000321165 ) ;
#4300=CARTESIAN_POINT ( 'NONE',  ( 17.00000000000000000, 25.00000000000000355, -195.0000000000000000 ) ) ;
#4301=EDGE_LOOP ( 'NONE', ( #5312, #5972, #5696, #80 ) ) ;
#4306=CIRCLE ( 'NONE', #6274, 90.00000000000000000 ) ;
#4307=DIRECTION ( 'NONE',  ( -0.000000000000000000, -0.000000000000000000, 1.000000000000000000 ) ) ;
#4309=VERTEX_POINT ( 'NONE', #5330 ) ;
#4310=CARTESIAN_POINT ( 'NONE',  ( 0.2052511266213280505, 21.25619793154159964, 15.00000000000000000 ) ) ;
#4314=EDGE_CURVE ( 'NONE', #5880, #3234, #5144, .T. ) ;
#4318=ORIENTED_EDGE ( 'NONE', *, *, #5437, .T. ) ;
#4319=CARTESIAN_POINT ( 'NONE',  ( -44.64065620456893413, -28.99954194078699032, -180.0000000000000000 ) ) ;
#4328=VERTEX_POINT ( 'NONE', #2389 ) ;
#4329=ORIENTED_EDGE ( 'NONE', *, *, #1260, .T. ) ;
#4335=ORIENTED_EDGE ( 'NONE', *, *, #2662, .F. ) ;
#4338=DIRECTION ( 'NONE',  ( -0.000000000000000000, -0.000000000000000000, 1.000000000000000000 ) ) ;
#4339=CYLINDRICAL_SURFACE ( 'NONE', #5976, 22.67164836619068424 ) ;
#4348=VERTEX_POINT ( 'NONE', #799 ) ;
#4353=EDGE_CURVE ( 'NONE', #427, #3554, #195, .T. ) ;
#4354=DIRECTION ( 'NONE',  ( -0.000000000000000000, -0.000000000000000000, 1.000000000000000000 ) ) ;
#4355=EDGE_CURVE ( 'NONE', #2452, #4562, #2135, .T. ) ;
#4356=CARTESIAN_POINT ( 'NONE',  ( 44.64065620456912598, 28.99954194078667413, -110.0000000000000000 ) ) ;
#4359=ORIENTED_EDGE ( 'NONE', *, *, #1630, .T. ) ;
#4362=EDGE_LOOP ( 'NONE', ( #5178, #1651, #474, #4185 ) ) ;
#4364=FACE_BOUND ( 'NONE', #1765, .T. ) ;
#4382=EDGE_CURVE ( 'NONE', #5613, #2780, #5179, .T. ) ;
#4391=FACE_OUTER_BOUND ( 'NONE', #5771, .T. ) ;
#4392=ORIENTED_EDGE ( 'NONE', *, *, #5908, .T. ) ;
#4393=ORIENTED_EDGE ( 'NONE', *, *, #189, .F. ) ;
#4396=ORIENTED_EDGE ( 'NONE', *, *, #189, .T. ) ;
#4397=EDGE_CURVE ( 'NONE', #1995, #768, #811, .T. ) ;
#4401=AXIS2_PLACEMENT_3D ( 'NONE', #918, #1335, #1914 ) ;
#4403=ORIENTED_EDGE ( 'NONE', *, *, #5169, .T. ) ;
#4405=ADVANCED_FACE ( 'NONE', ( #245, #2201 ), #4158, .F. ) ;
#4406=DIRECTION ( 'NONE',  ( 1.000000000000000000, 0.000000000000000000, 0.000000000000000000 ) ) ;
#4411=ORIENTED_EDGE ( 'NONE', *, *, #4637, .F. ) ;
#4414=ADVANCED_FACE ( 'NONE', ( #561 ), #3546, .T. ) ;
#4426=DIRECTION ( 'NONE',  ( 1.000000000000000000, 0.000000000000000000, 0.000000000000000000 ) ) ;
#4428=CARTESIAN_POINT ( 'NONE',  ( -17.00000000000000000, 25.00000000000000355, -30.00000000000000000 ) ) ;
#4431=ORIENTED_EDGE ( 'NONE', *, *, #5227, .F. ) ;
#4434=CARTESIAN_POINT ( 'NONE',  ( 17.00000000000000000, 0.000000000000000000, -273.0000000000000000 ) ) ;
#4438=MANIFOLD_SOLID_BREP ( 'Mirror10', #3190 ) ;
#4439=AXIS2_PLACEMENT_3D ( 'NONE', #229, #3944, #3007 ) ;
#4444=DIRECTION ( 'NONE',  ( -0.000000000000000000, -0.000000000000000000, -1.000000000000000000 ) ) ;
#4445=FACE_OUTER_BOUND ( 'NONE', #1955, .T. ) ;
#4449=EDGE_LOOP ( 'NONE', ( #3261, #6271 ) ) ;
#4452=FACE_OUTER_BOUND ( 'NONE', #2939, .T. ) ;
#4453=FACE_OUTER_BOUND ( 'NONE', #730, .T. ) ;
#4456=CARTESIAN_POINT ( 'NONE',  ( 44.00000000000000000, -13.41640786499874771, -240.0000000000000000 ) ) ;
#4459=ORIENTED_EDGE ( 'NONE', *, *, #4573, .T. ) ;
#4471=CARTESIAN_POINT ( 'NONE',  ( 2.380270672502711906E-15, -5.204170427930421283E-15, -180.0000000000000000 ) ) ;
#4476=ORIENTED_EDGE ( 'NONE', *, *, #801, .T. ) ;
#4482=DIRECTION ( 'NONE',  ( -1.000000000000000000, 0.000000000000000000, 0.000000000000000000 ) ) ;
#4483=EDGE_CURVE ( 'NONE', #624, #5536, #5973, .T. ) ;
#4487=AXIS2_PLACEMENT_3D ( 'NONE', #2794, #5666, #1249 ) ;
#4488=AXIS2_PLACEMENT_3D ( 'NONE', #1771, #3741, #3281 ) ;
#4489=DIRECTION ( 'NONE',  ( -1.000000000000000000, 0.000000000000000000, 0.000000000000000000 ) ) ;
#4490=DIRECTION ( 'NONE',  ( -0.000000000000000000, -0.000000000000000000, -1.000000000000000000 ) ) ;
#4492=DIRECTION ( 'NONE',  ( 1.000000000000000000, 0.000000000000000000, -0.000000000000000000 ) ) ;
#4494=AXIS2_PLACEMENT_3D ( 'NONE', #2742, #2296, #5720 ) ;
#4497=DIRECTION ( 'NONE',  ( -0.000000000000000000, -0.000000000000000000, 1.000000000000000000 ) ) ;
#4499=ORIENTED_EDGE ( 'NONE', *, *, #4833, .F. ) ;
#4500=AXIS2_PLACEMENT_3D ( 'NONE', #1085, #2666, #101 ) ;
#4502=AXIS2_PLACEMENT_3D ( 'NONE', #3386, #6352, #1202 ) ;
#4511=FACE_OUTER_BOUND ( 'NONE', #4738, .T. ) ;
#4512=AXIS2_PLACEMENT_3D ( 'NONE', #1049, #4490, #5406 ) ;
#4515=VERTEX_POINT ( 'NONE', #4993 ) ;
#4517=AXIS2_PLACEMENT_3D ( 'NONE', #6151, #2572, #750 ) ;
#4518=DIRECTION ( 'NONE',  ( -0.000000000000000000, -0.000000000000000000, -1.000000000000000000 ) ) ;
#4519=CARTESIAN_POINT ( 'NONE',  ( -44.64065620456893413, -28.99954194078699032, -30.00000000000000000 ) ) ;
#4521=CIRCLE ( 'NONE', #3505, 17.00000000000000000 ) ;
#4531=DIRECTION ( 'NONE',  ( 1.000000000000000000, 0.000000000000000000, 0.000000000000000000 ) ) ;
#4534=FACE_BOUND ( 'NONE', #2147, .T. ) ;
#4540=CARTESIAN_POINT ( 'NONE',  ( 0.000000000000000000, 0.000000000000000000, -248.0000000000000000 ) ) ;
#4541=VERTEX_POINT ( 'NONE', #3062 ) ;
#4542=EDGE_LOOP ( 'NONE', ( #3876, #2626, #226, #3402 ) ) ;
#4543=EDGE_LOOP ( 'NONE', ( #2399, #3623, #1037, #6342 ) ) ;
#4551=DIRECTION ( 'NONE',  ( 1.000000000000000000, 0.000000000000000000, 0.000000000000000000 ) ) ;
#4554=EDGE_CURVE ( 'NONE', #6160, #1758, #6157, .T. ) ;
#4559=CARTESIAN_POINT ( 'NONE',  ( -17.00000000000000000, 2.081899558550500280E-15, -248.0000000000000000 ) ) ;
#4560=ORIENTED_EDGE ( 'NONE', *, *, #5427, .T. ) ;
#4562=VERTEX_POINT ( 'NONE', #4141 ) ;
#4567=DIRECTION ( 'NONE',  ( -0.000000000000000000, 0.000000000000000000, -1.000000000000000000 ) ) ;
#4568=CARTESIAN_POINT ( 'NONE',  ( 0.2052511266213299934, 21.25619793154162807, -195.0000000000000000 ) ) ;
#4569=ORIENTED_EDGE ( 'NONE', *, *, #2077, .F. ) ;
#4570=DIRECTION ( 'NONE',  ( 0.000000000000000000, 0.000000000000000000, 1.000000000000000000 ) ) ;
#4573=EDGE_CURVE ( 'NONE', #3088, #4309, #204, .T. ) ;
#4574=CARTESIAN_POINT ( 'NONE',  ( -44.43364355155666345, 29.42304313293565343, -65.00000000000000000 ) ) ;
#4575=AXIS2_PLACEMENT_3D ( 'NONE', #6290, #1419, #3378 ) ;
#4578=ORIENTED_EDGE ( 'NONE', *, *, #4011, .F. ) ;
#4584=DIRECTION ( 'NONE',  ( -0.000000000000000000, -0.000000000000000000, -1.000000000000000000 ) ) ;
#4586=DIRECTION ( 'NONE',  ( 0.000000000000000000, 0.000000000000000000, 1.000000000000000000 ) ) ;
#4587=ORIENTED_EDGE ( 'NONE', *, *, #4124, .F. ) ;
#4590=ADVANCED_FACE ( 'NONE', ( #4665 ), #4218, .T. ) ;
#4592=AXIS2_PLACEMENT_3D ( 'NONE', #5046, #2917, #2411 ) ;
#4593=ORIENTED_EDGE ( 'NONE', *, *, #5559, .T. ) ;
#4595=ORIENTED_EDGE ( 'NONE', *, *, #4756, .T. ) ;
#4597=DIRECTION ( 'NONE',  ( -1.000000000000000000, 0.000000000000000000, 0.000000000000000000 ) ) ;
#4598=PLANE ( 'NONE',  #2894 ) ;
#4599=DIRECTION ( 'NONE',  ( 0.000000000000000000, 0.000000000000000000, 1.000000000000000000 ) ) ;
#4610=CARTESIAN_POINT ( 'NONE',  ( -16.23652742703189489, -37.28747423195188304, -130.0000000000000000 ) ) ;
#4613=VERTEX_POINT ( 'NONE', #4278 ) ;
#4615=DIRECTION ( 'NONE',  ( 1.000000000000000000, 0.000000000000000000, 0.000000000000000000 ) ) ;
#4618=CYLINDRICAL_SURFACE ( 'NONE', #1084, 22.67164836619067714 ) ;
#4621=CIRCLE ( 'NONE', #5549, 89.87058297576892585 ) ;
#4622=CYLINDRICAL_SURFACE ( 'NONE', #5854, 19.00000000000000000 ) ;
#4624=CARTESIAN_POINT ( 'NONE',  ( -2.385244779468109755E-15, -1.040834085586084257E-14, -110.0000000000000000 ) ) ;
#4625=CIRCLE ( 'NONE', #1641, 90.00000000000319744 ) ;
#4627=VERTEX_POINT ( 'NONE', #5780 ) ;
#4628=DIRECTION ( 'NONE',  ( 1.000000000000000000, 0.000000000000000000, 0.000000000000000000 ) ) ;
#4630=CARTESIAN_POINT ( 'NONE',  ( -19.00000000000000000, 0.000000000000000000, 15.00000000000000000 ) ) ;
#4632=FACE_OUTER_BOUND ( 'NONE', #2886, .T. ) ;
#4634=DIRECTION ( 'NONE',  ( 0.000000000000000000, 0.000000000000000000, -1.000000000000000000 ) ) ;
#4635=VERTEX_POINT ( 'NONE', #1381 ) ;
#4637=EDGE_CURVE ( 'NONE', #1077, #5724, #2352, .T. ) ;
#4640=DIRECTION ( 'NONE',  ( -0.000000000000000000, -0.000000000000000000, -1.000000000000000000 ) ) ;
#4641=CIRCLE ( 'NONE', #5473, 17.00000000000000000 ) ;
#4643=CARTESIAN_POINT ( 'NONE',  ( 13.14183123006952947, -39.58265509608667543, -65.00000000000000000 ) ) ;
#4645=VERTEX_POINT ( 'NONE', #3284 ) ;
#4646=CARTESIAN_POINT ( 'NONE',  ( 44.64065620456912598, 28.99954194078667413, -95.00000000000000000 ) ) ;
#4647=DIRECTION ( 'NONE',  ( -0.000000000000000000, -0.000000000000000000, -1.000000000000000000 ) ) ;
#4652=DIRECTION ( 'NONE',  ( 1.000000000000000000, 0.000000000000000000, 0.000000000000000000 ) ) ;
#4657=CARTESIAN_POINT ( 'NONE',  ( 0.000000000000000000, 0.000000000000000000, -273.0000000000000000 ) ) ;
#4659=DIRECTION ( 'NONE',  ( -0.000000000000000000, -0.000000000000000000, -1.000000000000000000 ) ) ;
#4661=DIRECTION ( 'NONE',  ( -0.000000000000000000, -0.000000000000000000, 1.000000000000000000 ) ) ;
#4665=FACE_OUTER_BOUND ( 'NONE', #652, .T. ) ;
#4671=EDGE_CURVE ( 'NONE', #2780, #3220, #2556, .T. ) ;
#4676=ADVANCED_FACE ( 'NONE', ( #1968 ), #3934, .T. ) ;
#4679=EDGE_CURVE ( 'NONE', #6010, #2034, #1426, .T. ) ;
#4680=CARTESIAN_POINT ( 'NONE',  ( 44.56092774862622719, -29.44644455561813956, 0.000000000000000000 ) ) ;
#4690=ORIENTED_EDGE ( 'NONE', *, *, #3467, .F. ) ;
#4694=DIRECTION ( 'NONE',  ( 0.000000000000000000, 0.000000000000000000, -1.000000000000000000 ) ) ;
#4695=VECTOR ( 'NONE', #2605, 1000.000000000000000 ) ;
#4699=DIRECTION ( 'NONE',  ( -1.000000000000000000, 0.000000000000000000, 0.000000000000000000 ) ) ;
#4701=AXIS2_PLACEMENT_3D ( 'NONE', #3374, #2378, #425 ) ;
#4705=CYLINDRICAL_SURFACE ( 'NONE', #3766, 89.87058297576894006 ) ;
#4706=CIRCLE ( 'NONE', #2844, 17.00000000000000000 ) ;
#4707=CARTESIAN_POINT ( 'NONE',  ( -15.82602517378898987, 37.28747423195201094, 15.00000000000000000 ) ) ;
#4712=LINE ( 'NONE', #4151, #1371 ) ;
#4714=DIRECTION ( 'NONE',  ( 0.000000000000000000, 0.000000000000000000, 1.000000000000000000 ) ) ;
#4715=CIRCLE ( 'NONE', #2051, 22.67164836619067714 ) ;
#4716=CARTESIAN_POINT ( 'NONE',  ( 22.21770253897382474, 3.871672004622519037, -115.0000000000000000 ) ) ;
#4717=EDGE_LOOP ( 'NONE', ( #1018, #20 ) ) ;
#4720=AXIS2_PLACEMENT_3D ( 'NONE', #2590, #3133, #4551 ) ;
#4721=CARTESIAN_POINT ( 'NONE',  ( 2.380270672502711906E-15, -5.204170427930421283E-15, -45.00000000000000000 ) ) ;
#4723=CARTESIAN_POINT ( 'NONE',  ( 0.000000000000000000, 0.000000000000000000, 48.00000000000000000 ) ) ;
#4725=EDGE_LOOP ( 'NONE', ( #3356, #5578, #3202, #1340 ) ) ;
#4729=ORIENTED_EDGE ( 'NONE', *, *, #2982, .T. ) ;
#4730=CIRCLE ( 'NONE', #3289, 90.00000000000319744 ) ;
#4732=DIRECTION ( 'NONE',  ( -0.000000000000000000, 0.000000000000000000, -1.000000000000000000 ) ) ;
#4738=EDGE_LOOP ( 'NONE', ( #5554, #6225, #4238, #798 ) ) ;
#4740=CARTESIAN_POINT ( 'NONE',  ( 44.00000000000009948, 13.41640786499835514, -110.0000000000000000 ) ) ;
#4741=CARTESIAN_POINT ( 'NONE',  ( 0.000000000000000000, 0.000000000000000000, 15.00000000000000000 ) ) ;
#4746=EDGE_LOOP ( 'NONE', ( #2900, #5585 ) ) ;
#4751=EDGE_CURVE ( 'NONE', #2498, #3061, #3069, .T. ) ;
#4755=ORIENTED_EDGE ( 'NONE', *, *, #4058, .T. ) ;
#4756=EDGE_CURVE ( 'NONE', #5184, #4635, #4715, .T. ) ;
#4762=ORIENTED_EDGE ( 'NONE', *, *, #327, .T. ) ;
#4765=CARTESIAN_POINT ( 'NONE',  ( -16.23652742703189489, -37.28747423195188304, -110.0000000000000000 ) ) ;
#4767=DIRECTION ( 'NONE',  ( 0.000000000000000000, 0.000000000000000000, -1.000000000000000000 ) ) ;
#4769=FACE_BOUND ( 'NONE', #3178, .T. ) ;
#4770=CARTESIAN_POINT ( 'NONE',  ( -0.2052511266214760433, -21.25619793154163517, -130.0000000000000000 ) ) ;
#4773=LINE ( 'NONE', #5677, #5390 ) ;
#4776=EDGE_LOOP ( 'NONE', ( #2325, #5952, #4392, #5725 ) ) ;
#4782=CARTESIAN_POINT ( 'NONE',  ( 22.21770253897382474, 3.871672004622519037, -65.00000000000000000 ) ) ;
#4783=VERTEX_POINT ( 'NONE', #3022 ) ;
#4787=CARTESIAN_POINT ( 'NONE',  ( 16.99999999999999645, -25.00000000000000000, -65.00000000000000000 ) ) ;
#4788=EDGE_LOOP ( 'NONE', ( #3269, #1581, #2164, #4227 ) ) ;
#4791=AXIS2_PLACEMENT_3D ( 'NONE', #2438, #3436, #1 ) ;
#4797=EDGE_LOOP ( 'NONE', ( #5836, #1954, #2652, #6193 ) ) ;
#4798=CIRCLE ( 'NONE', #4276, 89.87058297576892585 ) ;
#4799=CIRCLE ( 'NONE', #5624, 17.00000000000000000 ) ;
#4800=CIRCLE ( 'NONE', #3887, 46.00000000000000000 ) ;
#4811=DIRECTION ( 'NONE',  ( -1.000000000000000000, 0.000000000000000000, 0.000000000000000000 ) ) ;
#4815=VERTEX_POINT ( 'NONE', #3304 ) ;
#4819=LINE ( 'NONE', #3762, #4090 ) ;
#4825=AXIS2_PLACEMENT_3D ( 'NONE', #920, #2426, #3392 ) ;
#4826=CARTESIAN_POINT ( 'NONE',  ( -17.00000000000000000, 2.081899558550500280E-15, -49.99999999999999289 ) ) ;
#4828=CIRCLE ( 'NONE', #5656, 45.99999999999997868 ) ;
#4830=DIRECTION ( 'NONE',  ( -1.000000000000000000, 0.000000000000000000, 0.000000000000000000 ) ) ;
#4831=VERTEX_POINT ( 'NONE', #2843 ) ;
#4832=AXIS2_PLACEMENT_3D ( 'NONE', #3543, #977, #4868 ) ;
#4833=EDGE_CURVE ( 'NONE', #5651, #5709, #4819, .T. ) ;
#4834=CYLINDRICAL_SURFACE ( 'NONE', #2211, 17.00000000000000000 ) ;
#4836=AXIS2_PLACEMENT_3D ( 'NONE', #4657, #1597, #5535 ) ;
#4841=ORIENTED_EDGE ( 'NONE', *, *, #2469, .F. ) ;
#4843=DIRECTION ( 'NONE',  ( 1.000000000000000000, 0.000000000000000000, 0.000000000000000000 ) ) ;
#4844=VERTEX_POINT ( 'NONE', #6310 ) ;
#4845=AXIS2_PLACEMENT_3D ( 'NONE', #6142, #5664, #1245 ) ;
#4847=DIRECTION ( 'NONE',  ( 1.000000000000000000, 0.000000000000000000, -0.000000000000000000 ) ) ;
#4848=CARTESIAN_POINT ( 'NONE',  ( 0.000000000000000000, 0.000000000000000000, -45.00000000000000000 ) ) ;
#4850=ORIENTED_EDGE ( 'NONE', *, *, #3129, .T. ) ;
#4853=DIRECTION ( 'NONE',  ( 0.000000000000000000, 0.000000000000000000, -1.000000000000000000 ) ) ;
#4858=DIRECTION ( 'NONE',  ( 1.000000000000000000, 0.000000000000000000, -0.000000000000000000 ) ) ;
#4864=CIRCLE ( 'NONE', #350, 90.00000000000319744 ) ;
#4866=ADVANCED_FACE ( 'NONE', ( #4364, #1402 ), #3363, .T. ) ;
#4868=DIRECTION ( 'NONE',  ( 1.000000000000000000, 0.000000000000000000, -0.000000000000000000 ) ) ;
#4876=CARTESIAN_POINT ( 'NONE',  ( -0.2052511266214760433, -21.25619793154163517, -110.0000000000000000 ) ) ;
#4882=EDGE_LOOP ( 'NONE', ( #5215, #74, #5745, #186 ) ) ;
#4888=EDGE_LOOP ( 'NONE', ( #5403, #3384 ) ) ;
#4889=DIRECTION ( 'NONE',  ( -1.000000000000000000, 0.000000000000000000, 0.000000000000000000 ) ) ;
#4892=AXIS2_PLACEMENT_3D ( 'NONE', #5574, #98, #65 ) ;
#4895=ORIENTED_EDGE ( 'NONE', *, *, #5833, .T. ) ;
#4896=AXIS2_PLACEMENT_3D ( 'NONE', #120, #2194, #5519 ) ;
#4900=CARTESIAN_POINT ( 'NONE',  ( 0.000000000000000000, 0.000000000000000000, -49.99999999999999289 ) ) ;
#4907=CARTESIAN_POINT ( 'NONE',  ( 0.000000000000000000, 0.000000000000000000, -273.0000000000000000 ) ) ;
#4908=CIRCLE ( 'NONE', #4701, 90.00000000000319744 ) ;
#4910=DIRECTION ( 'NONE',  ( -0.000000000000000000, -0.000000000000000000, -1.000000000000000000 ) ) ;
#4912=EDGE_LOOP ( 'NONE', ( #5132, #3200, #1925, #4595 ) ) ;
#4918=AXIS2_PLACEMENT_3D ( 'NONE', #1014, #2974, #5917 ) ;
#4919=FACE_OUTER_BOUND ( 'NONE', #3093, .T. ) ;
#4922=DIRECTION ( 'NONE',  ( 0.000000000000000000, 0.000000000000000000, 1.000000000000000000 ) ) ;
#4925=CYLINDRICAL_SURFACE ( 'NONE', #2948, 22.67164836619068424 ) ;
#4927=DIRECTION ( 'NONE',  ( -1.000000000000000000, 0.000000000000000000, 0.000000000000000000 ) ) ;
#4928=ORIENTED_EDGE ( 'NONE', *, *, #3411, .T. ) ;
#4931=DIRECTION ( 'NONE',  ( -0.000000000000000000, -0.000000000000000000, -1.000000000000000000 ) ) ;
#4934=AXIS2_PLACEMENT_3D ( 'NONE', #631, #5888, #1579 ) ;
#4935=DIRECTION ( 'NONE',  ( 1.000000000000000000, 0.000000000000000000, 0.000000000000000000 ) ) ;
#4938=VERTEX_POINT ( 'NONE', #5043 ) ;
#4942=CARTESIAN_POINT ( 'NONE',  ( 16.23652742703164620, 37.28747423195200383, 15.00000000000000000 ) ) ;
#4946=CIRCLE ( 'NONE', #735, 89.87058297576894006 ) ;
#4951=CARTESIAN_POINT ( 'NONE',  ( 0.000000000000000000, 0.000000000000000000, -45.00000000000000000 ) ) ;
#4956=VERTEX_POINT ( 'NONE', #3466 ) ;
#4963=DIRECTION ( 'NONE',  ( 1.000000000000000000, 0.000000000000000000, 0.000000000000000000 ) ) ;
#4968=ORIENTED_EDGE ( 'NONE', *, *, #4353, .F. ) ;
#4973=AXIS2_PLACEMENT_3D ( 'NONE', #1843, #5166, #5783 ) ;
#4974=DIRECTION ( 'NONE',  ( -0.000000000000000000, 0.000000000000000000, -1.000000000000000000 ) ) ;
#4975=DIRECTION ( 'NONE',  ( -0.000000000000000000, 0.000000000000000000, -1.000000000000000000 ) ) ;
#4977=ORIENTED_EDGE ( 'NONE', *, *, #125, .F. ) ;
#4985=CYLINDRICAL_SURFACE ( 'NONE', #3598, 22.67164836619070911 ) ;
#4987=CARTESIAN_POINT ( 'NONE',  ( -0.2052511266214760433, -21.25619793154163517, -175.0000000000000284 ) ) ;
#4991=CARTESIAN_POINT ( 'NONE',  ( 0.000000000000000000, 25.00000000000000000, 0.000000000000000000 ) ) ;
#4993=CARTESIAN_POINT ( 'NONE',  ( 13.14183123006966980, -39.58265509608656174, -130.0000000000000000 ) ) ;
#5000=ORIENTED_EDGE ( 'NONE', *, *, #5504, .F. ) ;
#5009=ORIENTED_EDGE ( 'NONE', *, *, #3933, .F. ) ;
#5012=VECTOR ( 'NONE', #3909, 1000.000000000000000 ) ;
#5015=EDGE_CURVE ( 'NONE', #3955, #2906, #2456, .T. ) ;
#5017=VERTEX_POINT ( 'NONE', #3920 ) ;
#5018=ORIENTED_EDGE ( 'NONE', *, *, #6162, .T. ) ;
#5019=VECTOR ( 'NONE', #5291, 1000.000000000000000 ) ;
#5020=CARTESIAN_POINT ( 'NONE',  ( -3.061616997868383043E-15, -25.00000000000000000, -130.0000000000000000 ) ) ;
#5021=AXIS2_PLACEMENT_3D ( 'NONE', #2442, #4444, #2511 ) ;
#5024=EDGE_CURVE ( 'NONE', #3628, #4645, #4306, .T. ) ;
#5027=CARTESIAN_POINT ( 'NONE',  ( 16.23652742703164975, 37.28747423195200383, -45.00000000000000000 ) ) ;
#5028=EDGE_CURVE ( 'NONE', #1742, #5434, #205, .T. ) ;
#5031=ADVANCED_FACE ( 'NONE', ( #5955 ), #5894, .T. ) ;
#5032=EDGE_CURVE ( 'NONE', #5651, #5613, #5654, .T. ) ;
#5036=DIRECTION ( 'NONE',  ( -0.000000000000000000, -0.000000000000000000, -1.000000000000000000 ) ) ;
#5040=AXIS2_PLACEMENT_3D ( 'NONE', #4540, #1951, #4027 ) ;
#5041=CARTESIAN_POINT ( 'NONE',  ( -22.21770253897231839, -3.871672004621880436, -240.0000000000000000 ) ) ;
#5043=CARTESIAN_POINT ( 'NONE',  ( -17.00000000000000000, 25.00000000000000000, -225.0000000000000000 ) ) ;
#5044=EDGE_CURVE ( 'NONE', #4328, #157, #2524, .T. ) ;
#5046=CARTESIAN_POINT ( 'NONE',  ( -44.43364355155666345, 29.42304313293565343, -160.0000000000000284 ) ) ;
#5047=CARTESIAN_POINT ( 'NONE',  ( 17.00000000000000000, 2.081899558550500280E-15, 48.00000000000000000 ) ) ;
#5048=ORIENTED_EDGE ( 'NONE', *, *, #4751, .F. ) ;
#5053=AXIS2_PLACEMENT_3D ( 'NONE', #4143, #206, #1609 ) ;
#5062=ORIENTED_EDGE ( 'NONE', *, *, #3533, .F. ) ;
#5069=EDGE_CURVE ( 'NONE', #5434, #760, #4033, .T. ) ;
#5071=ORIENTED_EDGE ( 'NONE', *, *, #4184, .T. ) ;
#5073=ORIENTED_EDGE ( 'NONE', *, *, #4679, .T. ) ;
#5075=AXIS2_PLACEMENT_3D ( 'NONE', #2149, #3479, #4963 ) ;
#5077=DIRECTION ( 'NONE',  ( 0.000000000000000000, 0.000000000000000000, -1.000000000000000000 ) ) ;
#5078=EDGE_CURVE ( 'NONE', #5103, #4515, #764, .T. ) ;
#5084=EDGE_CURVE ( 'NONE', #2034, #5651, #5968, .T. ) ;
#5085=SHAPE_DEFINITION_REPRESENTATION ( #6113, #5199 ) ;
#5094=DIRECTION ( 'NONE',  ( -1.000000000000000000, 0.000000000000000000, 0.000000000000000000 ) ) ;
#5098=DIRECTION ( 'NONE',  ( -0.000000000000000000, -0.000000000000000000, -1.000000000000000000 ) ) ;
#5103=VERTEX_POINT ( 'NONE', #6078 ) ;
#5105=VERTEX_POINT ( 'NONE', #1712 ) ;
#5106=CARTESIAN_POINT ( 'NONE',  ( 0.000000000000000000, 25.00000000000000000, -30.00000000000000000 ) ) ;
#5107=CARTESIAN_POINT ( 'NONE',  ( 44.64065620456912598, 28.99954194078667413, -160.0000000000000284 ) ) ;
#5116=ORIENTED_EDGE ( 'NONE', *, *, #3127, .T. ) ;
#5118=ORIENTED_EDGE ( 'NONE', *, *, #3925, .F. ) ;
#5119=VECTOR ( 'NONE', #1748, 1000.000000000000000 ) ;
#5127=DIRECTION ( 'NONE',  ( -1.000000000000000000, 0.000000000000000000, 0.000000000000000000 ) ) ;
#5128=CARTESIAN_POINT ( 'NONE',  ( 2.380270672502711906E-15, -5.204170427930421283E-15, -30.00000000000000000 ) ) ;
#5129=AXIS2_PLACEMENT_3D ( 'NONE', #5367, #5813, #4843 ) ;
#5132=ORIENTED_EDGE ( 'NONE', *, *, #32, .T. ) ;
#5138=DIRECTION ( 'NONE',  ( 1.000000000000000000, 0.000000000000000000, 0.000000000000000000 ) ) ;
#5140=CARTESIAN_POINT ( 'NONE',  ( -43.99999999999990052, 13.41640786499905147, -65.00000000000000000 ) ) ;
#5142=LINE ( 'NONE', #4094, #619 ) ;
#5143=VECTOR ( 'NONE', #3159, 1000.000000000000000 ) ;
#5144=LINE ( 'NONE', #6296, #1528 ) ;
#5147=EDGE_CURVE ( 'NONE', #981, #3367, #569, .T. ) ;
#5148=CARTESIAN_POINT ( 'NONE',  ( -3.061616997868383043E-15, -25.00000000000000000, -160.0000000000000000 ) ) ;
#5149=VECTOR ( 'NONE', #6215, 1000.000000000000000 ) ;
#5157=CIRCLE ( 'NONE', #5371, 90.00000000000000000 ) ;
#5160=CARTESIAN_POINT ( 'NONE',  ( 0.000000000000000000, 25.00000000000000000, -195.0000000000000000 ) ) ;
#5161=EDGE_CURVE ( 'NONE', #306, #5596, #3385, .T. ) ;
#5162=DIRECTION ( 'NONE',  ( -0.000000000000000000, -0.000000000000000000, -1.000000000000000000 ) ) ;
#5166=DIRECTION ( 'NONE',  ( -0.000000000000000000, -0.000000000000000000, -1.000000000000000000 ) ) ;
#5168=CIRCLE ( 'NONE', #3612, 19.00000000000000000 ) ;
#5169=EDGE_CURVE ( 'NONE', #5213, #214, #2198, .T. ) ;
#5178=ORIENTED_EDGE ( 'NONE', *, *, #3013, .F. ) ;
#5179=LINE ( 'NONE', #6175, #2346 ) ;
#5180=ORIENTED_EDGE ( 'NONE', *, *, #1922, .F. ) ;
#5184=VERTEX_POINT ( 'NONE', #1756 ) ;
#5188=DIRECTION ( 'NONE',  ( -0.000000000000000000, 0.000000000000000000, -1.000000000000000000 ) ) ;
#5190=CARTESIAN_POINT ( 'NONE',  ( 0.000000000000000000, 25.00000000000000000, -30.00000000000000000 ) ) ;
#5191=ORIENTED_EDGE ( 'NONE', *, *, #3748, .F. ) ;
#5197=FACE_OUTER_BOUND ( 'NONE', #5787, .T. ) ;
#5199=SHAPE_REPRESENTATION ( 'Part 32,3_Varsay\X2\0131\X0\lan', ( #6349 ), #5524 ) ;
#5200=ORIENTED_EDGE ( 'NONE', *, *, #4483, .F. ) ;
#5203=DIRECTION ( 'NONE',  ( -0.000000000000000000, 0.000000000000000000, -1.000000000000000000 ) ) ;
#5204=CIRCLE ( 'NONE', #476, 17.00000000000000000 ) ;
#5205=FACE_OUTER_BOUND ( 'NONE', #1686, .T. ) ;
#5206=CIRCLE ( 'NONE', #4896, 90.00000000000000000 ) ;
#5208=DIRECTION ( 'NONE',  ( -0.000000000000000000, -0.000000000000000000, -1.000000000000000000 ) ) ;
#5210=CYLINDRICAL_SURFACE ( 'NONE', #1038, 17.00000000000000000 ) ;
#5212=CIRCLE ( 'NONE', #485, 17.00000000000000000 ) ;
#5213=VERTEX_POINT ( 'NONE', #5140 ) ;
#5215=ORIENTED_EDGE ( 'NONE', *, *, #4286, .F. ) ;
#5216=DIRECTION ( 'NONE',  ( -1.000000000000000000, 0.000000000000000000, 0.000000000000000000 ) ) ;
#5218=CARTESIAN_POINT ( 'NONE',  ( 44.43364355155687662, -29.42304313293534790, -45.00000000000000000 ) ) ;
#5223=ORIENTED_EDGE ( 'NONE', *, *, #3619, .T. ) ;
#5227=EDGE_CURVE ( 'NONE', #3307, #1044, #3075, .T. ) ;
#5229=ADVANCED_FACE ( 'NONE', ( #2105 ), #1269, .T. ) ;
#5232=EDGE_CURVE ( 'NONE', #2249, #6115, #1950, .T. ) ;
#5236=EDGE_CURVE ( 'NONE', #4541, #738, #5551, .T. ) ;
#5238=DIRECTION ( 'NONE',  ( -0.000000000000000000, -0.000000000000000000, -1.000000000000000000 ) ) ;
#5242=ORIENTED_EDGE ( 'NONE', *, *, #1148, .T. ) ;
#5246=CYLINDRICAL_SURFACE ( 'NONE', #329, 46.00000000000000000 ) ;
#5251=DIRECTION ( 'NONE',  ( -0.000000000000000000, -0.000000000000000000, 1.000000000000000000 ) ) ;
#5254=DIRECTION ( 'NONE',  ( -0.000000000000000000, -0.000000000000000000, 1.000000000000000000 ) ) ;
#5256=CARTESIAN_POINT ( 'NONE',  ( 0.000000000000000000, 0.000000000000000000, -65.00000000000000000 ) ) ;
#5258=CIRCLE ( 'NONE', #2367, 46.00000000000000000 ) ;
#5262=ORIENTED_EDGE ( 'NONE', *, *, #4397, .T. ) ;
#5265=CARTESIAN_POINT ( 'NONE',  ( -15.82602517378898987, 37.28747423195201094, -240.0000000000000000 ) ) ;
#5279=CYLINDRICAL_SURFACE ( 'NONE', #3693, 89.99999999999998579 ) ;
#5283=CARTESIAN_POINT ( 'NONE',  ( 44.00000000000008527, 13.41640786499836224, -175.0000000000000284 ) ) ;
#5290=CARTESIAN_POINT ( 'NONE',  ( 44.64065620456912598, 28.99954194078667413, -49.99999999999999289 ) ) ;
#5291=DIRECTION ( 'NONE',  ( -0.000000000000000000, -0.000000000000000000, -1.000000000000000000 ) ) ;
#5293=EDGE_LOOP ( 'NONE', ( #1363, #971, #4476, #978 ) ) ;
#5296=PLANE ( 'NONE',  #3570 ) ;
#5299=VERTEX_POINT ( 'NONE', #410 ) ;
#5301=CARTESIAN_POINT ( 'NONE',  ( 16.23652742703164620, 37.28747423195200383, -240.0000000000000000 ) ) ;
#5302=CARTESIAN_POINT ( 'NONE',  ( 44.00000000000009948, 13.41640786499835514, -115.0000000000000000 ) ) ;
#5303=ADVANCED_FACE ( 'NONE', ( #2811 ), #3785, .T. ) ;
#5304=FACE_BOUND ( 'NONE', #3003, .T. ) ;
#5311=LINE ( 'NONE', #325, #5149 ) ;
#5312=ORIENTED_EDGE ( 'NONE', *, *, #2923, .F. ) ;
#5315=EDGE_CURVE ( 'NONE', #1044, #3307, #2032, .T. ) ;
#5319=DIRECTION ( 'NONE',  ( 1.000000000000000000, 0.000000000000000000, 0.000000000000000000 ) ) ;
#5320=DIRECTION ( 'NONE',  ( 1.000000000000000000, 0.000000000000000000, 0.000000000000000000 ) ) ;
#5322=AXIS2_PLACEMENT_3D ( 'NONE', #2647, #3196, #1166 ) ;
#5325=CARTESIAN_POINT ( 'NONE',  ( 19.00000000000000000, 0.000000000000000000, -248.0000000000000000 ) ) ;
#5327=AXIS2_PLACEMENT_3D ( 'NONE', #715, #3148, #3213 ) ;
#5330=CARTESIAN_POINT ( 'NONE',  ( -16.23652742703190199, -37.28747423195189015, -49.99999999999999289 ) ) ;
#5332=CARTESIAN_POINT ( 'NONE',  ( 0.000000000000000000, 0.000000000000000000, -49.99999999999999289 ) ) ;
#5333=CIRCLE ( 'NONE', #3471, 17.00000000000000000 ) ;
#5337=CIRCLE ( 'NONE', #293, 17.00000000000000000 ) ;
#5339=ORIENTED_EDGE ( 'NONE', *, *, #4554, .T. ) ;
#5346=VERTEX_POINT ( 'NONE', #1298 ) ;
#5358=ADVANCED_FACE ( 'NONE', ( #2331 ), #4291, .T. ) ;
#5360=AXIS2_PLACEMENT_3D ( 'NONE', #1676, #3098, #1160 ) ;
#5361=CYLINDRICAL_SURFACE ( 'NONE', #1589, 17.00000000000000000 ) ;
#5363=EDGE_CURVE ( 'NONE', #6115, #157, #5636, .T. ) ;
#5367=CARTESIAN_POINT ( 'NONE',  ( 0.000000000000000000, 0.000000000000000000, 15.00000000000000000 ) ) ;
#5369=DIRECTION ( 'NONE',  ( -0.000000000000000000, -0.000000000000000000, -1.000000000000000000 ) ) ;
#5371=AXIS2_PLACEMENT_3D ( 'NONE', #4200, #3729, #803 ) ;
#5373=FACE_BOUND ( 'NONE', #1750, .T. ) ;
#5374=FACE_OUTER_BOUND ( 'NONE', #260, .T. ) ;
#5375=ORIENTED_EDGE ( 'NONE', *, *, #4058, .F. ) ;
#5380=AXIS2_PLACEMENT_3D ( 'NONE', #2210, #6147, #1734 ) ;
#5383=DIRECTION ( 'NONE',  ( -0.000000000000000000, -0.000000000000000000, -1.000000000000000000 ) ) ;
#5390=VECTOR ( 'NONE', #367, 1000.000000000000000 ) ;
#5398=CARTESIAN_POINT ( 'NONE',  ( 0.000000000000000000, 0.000000000000000000, -240.0000000000000000 ) ) ;
#5403=ORIENTED_EDGE ( 'NONE', *, *, #3338, .F. ) ;
#5406=DIRECTION ( 'NONE',  ( 1.000000000000000000, 0.000000000000000000, 0.000000000000000000 ) ) ;
#5409=CARTESIAN_POINT ( 'NONE',  ( -22.21770253897231839, -3.871672004621880436, 15.00000000000000000 ) ) ;
#5412=VECTOR ( 'NONE', #3315, 1000.000000000000000 ) ;
#5413=DIRECTION ( 'NONE',  ( -0.000000000000000000, -0.000000000000000000, -1.000000000000000000 ) ) ;
#5415=AXIS2_PLACEMENT_3D ( 'NONE', #2024, #3049, #5475 ) ;
#5416=DIRECTION ( 'NONE',  ( -1.000000000000000000, 0.000000000000000000, 0.000000000000000000 ) ) ;
#5420=CIRCLE ( 'NONE', #383, 17.00000000000000000 ) ;
#5426=EDGE_CURVE ( 'NONE', #1338, #2268, #3672, .T. ) ;
#5427=EDGE_CURVE ( 'NONE', #4122, #4938, #5333, .T. ) ;
#5428=FACE_BOUND ( 'NONE', #178, .T. ) ;
#5431=DIRECTION ( 'NONE',  ( -0.000000000000000000, -0.000000000000000000, 1.000000000000000000 ) ) ;
#5434=VERTEX_POINT ( 'NONE', #5302 ) ;
#5437=EDGE_CURVE ( 'NONE', #768, #5105, #704, .T. ) ;
#5444=AXIS2_PLACEMENT_3D ( 'NONE', #220, #1587, #1563 ) ;
#5450=CARTESIAN_POINT ( 'NONE',  ( 0.000000000000000000, 0.000000000000000000, 23.00000000000000000 ) ) ;
#5461=LINE ( 'NONE', #2009, #4289 ) ;
#5468=CARTESIAN_POINT ( 'NONE',  ( -0.2052511266214760433, -21.25619793154163517, -115.0000000000000000 ) ) ;
#5471=ORIENTED_EDGE ( 'NONE', *, *, #4268, .T. ) ;
#5473=AXIS2_PLACEMENT_3D ( 'NONE', #6059, #2454, #1694 ) ;
#5475=DIRECTION ( 'NONE',  ( 1.000000000000000000, 0.000000000000000000, 0.000000000000000000 ) ) ;
#5476=FACE_OUTER_BOUND ( 'NONE', #19, .T. ) ;
#5479=FACE_OUTER_BOUND ( 'NONE', #2116, .T. ) ;
#5480=DIRECTION ( 'NONE',  ( 0.000000000000000000, 0.000000000000000000, -1.000000000000000000 ) ) ;
#5484=DIRECTION ( 'NONE',  ( -0.000000000000000000, -0.000000000000000000, -1.000000000000000000 ) ) ;
#5488=ORIENTED_EDGE ( 'NONE', *, *, #5315, .T. ) ;
#5489=EDGE_LOOP ( 'NONE', ( #342, #3793, #5584, #1193 ) ) ;
#5491=VERTEX_POINT ( 'NONE', #49 ) ;
#5495=LINE ( 'NONE', #5047, #5646 ) ;
#5497=ADVANCED_FACE ( 'NONE', ( #5887 ), #507, .T. ) ;
#5500=ADVANCED_FACE ( 'NONE', ( #4511, #5373 ), #1982, .T. ) ;
#5502=ORIENTED_EDGE ( 'NONE', *, *, #5024, .T. ) ;
#5504=EDGE_CURVE ( 'NONE', #1044, #4562, #5461, .T. ) ;
#5509=VERTEX_POINT ( 'NONE', #467 ) ;
#5510=CARTESIAN_POINT ( 'NONE',  ( -3.061616997868383043E-15, -25.00000000000000000, -95.00000000000000000 ) ) ;
#5519=DIRECTION ( 'NONE',  ( -1.000000000000000000, 0.000000000000000000, 0.000000000000000000 ) ) ;
#5524=( GEOMETRIC_REPRESENTATION_CONTEXT ( 3 ) GLOBAL_UNCERTAINTY_ASSIGNED_CONTEXT ( ( #4168 ) ) GLOBAL_UNIT_ASSIGNED_CONTEXT ( ( #1280, #2754, #6118 ) ) REPRESENTATION_CONTEXT ( 'NONE', 'WORKASPACE' ) );
#5525=DIRECTION ( 'NONE',  ( 1.000000000000000000, 0.000000000000000000, 0.000000000000000000 ) ) ;
#5530=CIRCLE ( 'NONE', #5750, 19.00000000000000000 ) ;
#5533=EDGE_CURVE ( 'NONE', #4831, #5346, #4706, .T. ) ;
#5535=DIRECTION ( 'NONE',  ( 1.000000000000000000, 0.000000000000000000, 0.000000000000000000 ) ) ;
#5536=VERTEX_POINT ( 'NONE', #1526 ) ;
#5537=AXIS2_PLACEMENT_3D ( 'NONE', #278, #1882, #2746 ) ;
#5538=CARTESIAN_POINT ( 'NONE',  ( -3.061616997868383043E-15, -25.00000000000000000, -95.00000000000000000 ) ) ;
#5540=CARTESIAN_POINT ( 'NONE',  ( 0.2052511266213299934, 21.25619793154162807, -45.00000000000000000 ) ) ;
#5543=EDGE_LOOP ( 'NONE', ( #5673, #2846 ) ) ;
#5545=AXIS2_PLACEMENT_3D ( 'NONE', #6045, #734, #4155 ) ;
#5549=AXIS2_PLACEMENT_3D ( 'NONE', #6269, #3875, #2777 ) ;
#5551=CIRCLE ( 'NONE', #3082, 17.00000000000000000 ) ;
#5552=CARTESIAN_POINT ( 'NONE',  ( -43.99999999999990052, 13.41640786499905147, -160.0000000000000284 ) ) ;
#5554=ORIENTED_EDGE ( 'NONE', *, *, #1731, .F. ) ;
#5555=ORIENTED_EDGE ( 'NONE', *, *, #6292, .F. ) ;
#5556=VERTEX_POINT ( 'NONE', #6005 ) ;
#5559=EDGE_CURVE ( 'NONE', #768, #5017, #2455, .T. ) ;
#5563=CARTESIAN_POINT ( 'NONE',  ( 16.23652742703164975, 37.28747423195200383, -195.0000000000000000 ) ) ;
#5564=DIRECTION ( 'NONE',  ( -1.000000000000000000, 0.000000000000000000, 0.000000000000000000 ) ) ;
#5566=PRODUCT_CONTEXT ( 'NONE', #1590, 'mechanical' ) ;
#5569=CIRCLE ( 'NONE', #3815, 46.00000000000000000 ) ;
#5574=CARTESIAN_POINT ( 'NONE',  ( 44.64065620456912598, 28.99954194078667413, -130.0000000000000000 ) ) ;
#5576=CYLINDRICAL_SURFACE ( 'NONE', #5840, 17.00000000000000000 ) ;
#5578=ORIENTED_EDGE ( 'NONE', *, *, #6105, .T. ) ;
#5580=CARTESIAN_POINT ( 'NONE',  ( 44.00000000000000000, -13.41640786499874771, 0.000000000000000000 ) ) ;
#5584=ORIENTED_EDGE ( 'NONE', *, *, #3324, .F. ) ;
#5585=ORIENTED_EDGE ( 'NONE', *, *, #3601, .T. ) ;
#5591=DIRECTION ( 'NONE',  ( -0.000000000000000000, 0.000000000000000000, -1.000000000000000000 ) ) ;
#5596=VERTEX_POINT ( 'NONE', #3189 ) ;
#5599=ORIENTED_EDGE ( 'NONE', *, *, #5147, .F. ) ;
#5602=CARTESIAN_POINT ( 'NONE',  ( 44.00000000000000000, -13.41640786499873705, -30.00000000000000000 ) ) ;
#5604=CARTESIAN_POINT ( 'NONE',  ( -43.99999999999987921, 13.41640786499904969, -115.0000000000000000 ) ) ;
#5610=DIRECTION ( 'NONE',  ( -0.000000000000000000, -0.000000000000000000, -1.000000000000000000 ) ) ;
#5613=VERTEX_POINT ( 'NONE', #1648 ) ;
#5614=EDGE_CURVE ( 'NONE', #4645, #1019, #1159, .T. ) ;
#5621=DIRECTION ( 'NONE',  ( 1.000000000000000000, 0.000000000000000000, 0.000000000000000000 ) ) ;
#5623=VECTOR ( 'NONE', #887, 1000.000000000000000 ) ;
#5624=AXIS2_PLACEMENT_3D ( 'NONE', #2177, #2664, #6185 ) ;
#5626=DIRECTION ( 'NONE',  ( 0.000000000000000000, 0.000000000000000000, -1.000000000000000000 ) ) ;
#5627=ORIENTED_EDGE ( 'NONE', *, *, #2548, .F. ) ;
#5636=CIRCLE ( 'NONE', #3268, 46.00000000000000000 ) ;
#5637=LINE ( 'NONE', #4765, #1601 ) ;
#5641=LINE ( 'NONE', #5604, #2871 ) ;
#5646=VECTOR ( 'NONE', #2107, 1000.000000000000000 ) ;
#5651=VERTEX_POINT ( 'NONE', #882 ) ;
#5653=AXIS2_PLACEMENT_3D ( 'NONE', #2650, #244, #275 ) ;
#5654=CIRCLE ( 'NONE', #4512, 22.67164836619068424 ) ;
#5655=CARTESIAN_POINT ( 'NONE',  ( 44.00000000000009948, 13.41640786499835514, -130.0000000000000000 ) ) ;
#5656=AXIS2_PLACEMENT_3D ( 'NONE', #4624, #2654, #3653 ) ;
#5661=VERTEX_POINT ( 'NONE', #1879 ) ;
#5664=DIRECTION ( 'NONE',  ( 0.000000000000000000, 0.000000000000000000, 1.000000000000000000 ) ) ;
#5666=DIRECTION ( 'NONE',  ( -0.000000000000000000, 0.000000000000000000, -1.000000000000000000 ) ) ;
#5667=CIRCLE ( 'NONE', #2782, 22.67164836619067714 ) ;
#5670=DIRECTION ( 'NONE',  ( -0.000000000000000000, -0.000000000000000000, -1.000000000000000000 ) ) ;
#5671=PRODUCT_DEFINITION_CONTEXT ( 'detailed design', #2379, 'design' ) ;
#5673=ORIENTED_EDGE ( 'NONE', *, *, #2577, .T. ) ;
#5677=CARTESIAN_POINT ( 'NONE',  ( -44.00000000000000000, -13.41640786499873350, -180.0000000000000000 ) ) ;
#5683=DIRECTION ( 'NONE',  ( -1.000000000000000000, 0.000000000000000000, 0.000000000000000000 ) ) ;
#5687=ORIENTED_EDGE ( 'NONE', *, *, #5015, .T. ) ;
#5689=ORIENTED_EDGE ( 'NONE', *, *, #5363, .F. ) ;
#5695=DIRECTION ( 'NONE',  ( -0.000000000000000000, -0.000000000000000000, -1.000000000000000000 ) ) ;
#5696=ORIENTED_EDGE ( 'NONE', *, *, #6292, .T. ) ;
#5697=EDGE_CURVE ( 'NONE', #4562, #2452, #5530, .T. ) ;
#5701=CARTESIAN_POINT ( 'NONE',  ( -17.00000000000000000, 25.00000000000000355, 0.000000000000000000 ) ) ;
#5702=DIRECTION ( 'NONE',  ( -1.000000000000000000, 0.000000000000000000, 0.000000000000000000 ) ) ;
#5706=EDGE_CURVE ( 'NONE', #3426, #1557, #1516, .T. ) ;
#5709=VERTEX_POINT ( 'NONE', #6197 ) ;
#5710=DIRECTION ( 'NONE',  ( -0.000000000000000000, -0.000000000000000000, 1.000000000000000000 ) ) ;
#5711=CARTESIAN_POINT ( 'NONE',  ( -17.00000000000000000, 25.00000000000000355, -30.00000000000000000 ) ) ;
#5714=ORIENTED_EDGE ( 'NONE', *, *, #5169, .F. ) ;
#5716=EDGE_CURVE ( 'NONE', #981, #2906, #1777, .T. ) ;
#5717=ORIENTED_EDGE ( 'NONE', *, *, #517, .T. ) ;
#5720=DIRECTION ( 'NONE',  ( 1.000000000000000000, 0.000000000000000000, 0.000000000000000000 ) ) ;
#5721=AXIS2_PLACEMENT_3D ( 'NONE', #5020, #2569, #1032 ) ;
#5724=VERTEX_POINT ( 'NONE', #4707 ) ;
#5725=ORIENTED_EDGE ( 'NONE', *, *, #3533, .T. ) ;
#5736=CIRCLE ( 'NONE', #5327, 45.99999999999997868 ) ;
#5737=ADVANCED_FACE ( 'NONE', ( #3779, #3316 ), #5296, .T. ) ;
#5739=DIRECTION ( 'NONE',  ( -0.000000000000000000, 0.000000000000000000, -1.000000000000000000 ) ) ;
#5740=CARTESIAN_POINT ( 'NONE',  ( 0.000000000000000000, 0.000000000000000000, -160.0000000000000284 ) ) ;
#5745=ORIENTED_EDGE ( 'NONE', *, *, #5084, .F. ) ;
#5750=AXIS2_PLACEMENT_3D ( 'NONE', #4741, #909, #2731 ) ;
#5751=CARTESIAN_POINT ( 'NONE',  ( 0.000000000000000000, 0.000000000000000000, -248.0000000000000000 ) ) ;
#5768=CIRCLE ( 'NONE', #3803, 19.00000000000000000 ) ;
#5769=ORIENTED_EDGE ( 'NONE', *, *, #2570, .T. ) ;
#5771=EDGE_LOOP ( 'NONE', ( #3240, #4217, #5627, #960 ) ) ;
#5775=CARTESIAN_POINT ( 'NONE',  ( -44.43364355155666345, 29.42304313293564988, -95.00000000000000000 ) ) ;
#5780=CARTESIAN_POINT ( 'NONE',  ( -16.23652742703189489, -37.28747423195188304, -95.00000000000000000 ) ) ;
#5783=DIRECTION ( 'NONE',  ( -1.000000000000000000, 0.000000000000000000, 0.000000000000000000 ) ) ;
#5784=CARTESIAN_POINT ( 'NONE',  ( -17.00000000000000355, -24.99999999999999645, -95.00000000000000000 ) ) ;
#5786=ORIENTED_EDGE ( 'NONE', *, *, #4124, .T. ) ;
#5787=EDGE_LOOP ( 'NONE', ( #5242, #5223, #3036, #3914 ) ) ;
#5789=VECTOR ( 'NONE', #2836, 1000.000000000000000 ) ;
#5791=DIRECTION ( 'NONE',  ( -0.000000000000000000, -0.000000000000000000, -1.000000000000000000 ) ) ;
#5792=DIRECTION ( 'NONE',  ( -0.000000000000000000, -0.000000000000000000, 1.000000000000000000 ) ) ;
#5803=FACE_OUTER_BOUND ( 'NONE', #1787, .T. ) ;
#5806=EDGE_LOOP ( 'NONE', ( #1570, #567, #830, #4258 ) ) ;
#5811=ORIENTED_EDGE ( 'NONE', *, *, #1330, .T. ) ;
#5812=EDGE_CURVE ( 'NONE', #214, #2898, #2221, .T. ) ;
#5813=DIRECTION ( 'NONE',  ( 0.000000000000000000, 0.000000000000000000, 1.000000000000000000 ) ) ;
#5814=ORIENTED_EDGE ( 'NONE', *, *, #483, .F. ) ;
#5816=LINE ( 'NONE', #4290, #5623 ) ;
#5821=ORIENTED_EDGE ( 'NONE', *, *, #5015, .F. ) ;
#5829=EDGE_LOOP ( 'NONE', ( #6360, #5118, #3763, #2534 ) ) ;
#5831=FACE_OUTER_BOUND ( 'NONE', #3475, .T. ) ;
#5833=EDGE_CURVE ( 'NONE', #427, #5346, #3000, .T. ) ;
#5835=CARTESIAN_POINT ( 'NONE',  ( -15.82602517378898987, 37.28747423195201094, -240.0000000000000000 ) ) ;
#5836=ORIENTED_EDGE ( 'NONE', *, *, #2936, .F. ) ;
#5837=EDGE_CURVE ( 'NONE', #3260, #5184, #2924, .T. ) ;
#5838=AXIS2_PLACEMENT_3D ( 'NONE', #5468, #4057, #6044 ) ;
#5840=AXIS2_PLACEMENT_3D ( 'NONE', #5160, #2571, #5094 ) ;
#5841=CARTESIAN_POINT ( 'NONE',  ( 0.000000000000000000, 0.000000000000000000, -273.0000000000000000 ) ) ;
#5851=FACE_OUTER_BOUND ( 'NONE', #2216, .T. ) ;
#5854=AXIS2_PLACEMENT_3D ( 'NONE', #4035, #127, #642 ) ;
#5855=AXIS2_PLACEMENT_3D ( 'NONE', #810, #4307, #5319 ) ;
#5864=ORIENTED_EDGE ( 'NONE', *, *, #5437, .F. ) ;
#5865=VECTOR ( 'NONE', #6169, 1000.000000000000000 ) ;
#5866=CARTESIAN_POINT ( 'NONE',  ( 0.000000000000000000, 0.000000000000000000, -49.99999999999999289 ) ) ;
#5867=CIRCLE ( 'NONE', #97, 90.00000000000000000 ) ;
#5871=AXIS2_PLACEMENT_3D ( 'NONE', #5148, #2686, #2783 ) ;
#5874=ORIENTED_EDGE ( 'NONE', *, *, #662, .F. ) ;
#5876=AXIS2_PLACEMENT_3D ( 'NONE', #4574, #3125, #658 ) ;
#5878=DIRECTION ( 'NONE',  ( -0.000000000000000000, -0.000000000000000000, -1.000000000000000000 ) ) ;
#5879=CARTESIAN_POINT ( 'NONE',  ( 16.99999999999999645, -25.00000000000000000, -95.00000000000000000 ) ) ;
#5880=VERTEX_POINT ( 'NONE', #41 ) ;
#5881=DIRECTION ( 'NONE',  ( -0.000000000000000000, -0.000000000000000000, 1.000000000000000000 ) ) ;
#5885=CIRCLE ( 'NONE', #3975, 17.00000000000000000 ) ;
#5886=FACE_BOUND ( 'NONE', #5543, .T. ) ;
#5887=FACE_OUTER_BOUND ( 'NONE', #543, .T. ) ;
#5888=DIRECTION ( 'NONE',  ( -0.000000000000000000, -0.000000000000000000, -1.000000000000000000 ) ) ;
#5894=CYLINDRICAL_SURFACE ( 'NONE', #3695, 17.00000000000000000 ) ;
#5897=DIRECTION ( 'NONE',  ( 0.000000000000000000, 0.000000000000000000, 1.000000000000000000 ) ) ;
#5898=CARTESIAN_POINT ( 'NONE',  ( 22.21770253897382474, 3.871672004622519037, -110.0000000000000000 ) ) ;
#5900=FACE_OUTER_BOUND ( 'NONE', #3734, .T. ) ;
#5903=DIRECTION ( 'NONE',  ( 0.000000000000000000, 0.000000000000000000, -1.000000000000000000 ) ) ;
#5904=EDGE_CURVE ( 'NONE', #2498, #5491, #3482, .T. ) ;
#5908=EDGE_CURVE ( 'NONE', #760, #4515, #1088, .T. ) ;
#5909=EDGE_CURVE ( 'NONE', #1953, #2336, #1117, .T. ) ;
#5917=DIRECTION ( 'NONE',  ( 1.000000000000000000, 0.000000000000000000, -0.000000000000000000 ) ) ;
#5918=CARTESIAN_POINT ( 'NONE',  ( 44.64065620456912598, 28.99954194078667413, -65.00000000000000000 ) ) ;
#5920=EDGE_CURVE ( 'NONE', #3208, #624, #5956, .T. ) ;
#5921=ORIENTED_EDGE ( 'NONE', *, *, #2271, .F. ) ;
#5923=ORIENTED_EDGE ( 'NONE', *, *, #801, .F. ) ;
#5924=DIRECTION ( 'NONE',  ( -0.000000000000000000, 0.000000000000000000, -1.000000000000000000 ) ) ;
#5925=DIRECTION ( 'NONE',  ( -1.000000000000000000, 0.000000000000000000, 0.000000000000000000 ) ) ;
#5930=EDGE_CURVE ( 'NONE', #738, #4541, #1923, .T. ) ;
#5932=ORIENTED_EDGE ( 'NONE', *, *, #108, .T. ) ;
#5933=ORIENTED_EDGE ( 'NONE', *, *, #4637, .T. ) ;
#5936=FACE_OUTER_BOUND ( 'NONE', #4362, .T. ) ;
#5939=AXIS2_PLACEMENT_3D ( 'NONE', #5107, #5238, #2262 ) ;
#5942=PLANE ( 'NONE',  #4832 ) ;
#5947=DIRECTION ( 'NONE',  ( 1.000000000000000000, 0.000000000000000000, 0.000000000000000000 ) ) ;
#5948=CARTESIAN_POINT ( 'NONE',  ( -22.21770253897231839, -3.871672004621880436, -225.0000000000000000 ) ) ;
#5951=ORIENTED_EDGE ( 'NONE', *, *, #5032, .T. ) ;
#5952=ORIENTED_EDGE ( 'NONE', *, *, #4211, .T. ) ;
#5955=FACE_OUTER_BOUND ( 'NONE', #3974, .T. ) ;
#5956=CIRCLE ( 'NONE', #591, 22.67164836619068424 ) ;
#5959=AXIS2_PLACEMENT_3D ( 'NONE', #5991, #2560, #5564 ) ;
#5960=DIRECTION ( 'NONE',  ( 1.000000000000000000, 0.000000000000000000, 0.000000000000000000 ) ) ;
#5962=AXIS2_PLACEMENT_3D ( 'NONE', #4310, #2284, #1875 ) ;
#5967=DIRECTION ( 'NONE',  ( 0.000000000000000000, 0.000000000000000000, -1.000000000000000000 ) ) ;
#5968=CIRCLE ( 'NONE', #416, 89.87058297576894006 ) ;
#5970=VECTOR ( 'NONE', #1086, 1000.000000000000000 ) ;
#5971=LINE ( 'NONE', #3989, #1337 ) ;
#5972=ORIENTED_EDGE ( 'NONE', *, *, #752, .F. ) ;
#5973=LINE ( 'NONE', #5027, #3486 ) ;
#5976=AXIS2_PLACEMENT_3D ( 'NONE', #3340, #2854, #4830 ) ;
#5977=DIRECTION ( 'NONE',  ( 1.000000000000000000, 0.000000000000000000, 0.000000000000000000 ) ) ;
#5991=CARTESIAN_POINT ( 'NONE',  ( 44.64065620456912598, 28.99954194078667413, -115.0000000000000000 ) ) ;
#5992=ORIENTED_EDGE ( 'NONE', *, *, #1232, .F. ) ;
#5993=AXIS2_PLACEMENT_3D ( 'NONE', #5948, #4767, #6251 ) ;
#5994=CARTESIAN_POINT ( 'NONE',  ( -44.00000000000000000, -13.41640786499873350, -195.0000000000000000 ) ) ;
#5997=DIRECTION ( 'NONE',  ( 1.000000000000000000, 0.000000000000000000, 0.000000000000000000 ) ) ;
#5999=FACE_OUTER_BOUND ( 'NONE', #347, .T. ) ;
#6005=CARTESIAN_POINT ( 'NONE',  ( -17.00000000000000000, 0.000000000000000000, -175.0000000000000284 ) ) ;
#6006=ADVANCED_FACE ( 'NONE', ( #1216 ), #5576, .T. ) ;
#6007=DIRECTION ( 'NONE',  ( 1.000000000000000000, 0.000000000000000000, 0.000000000000000000 ) ) ;
#6010=VERTEX_POINT ( 'NONE', #3569 ) ;
#6012=EDGE_CURVE ( 'NONE', #1881, #4328, #4800, .T. ) ;
#6037=CARTESIAN_POINT ( 'NONE',  ( -13.14183123006980480, 39.58265509608657595, -45.00000000000000000 ) ) ;
#6042=PLANE ( 'NONE',  #1567 ) ;
#6044=DIRECTION ( 'NONE',  ( -1.000000000000000000, 0.000000000000000000, 0.000000000000000000 ) ) ;
#6045=CARTESIAN_POINT ( 'NONE',  ( 0.2052511266213280505, 21.25619793154159964, -240.0000000000000000 ) ) ;
#6048=CARTESIAN_POINT ( 'NONE',  ( -13.14183123006980480, 39.58265509608657595, -30.00000000000000000 ) ) ;
#6055=ORIENTED_EDGE ( 'NONE', *, *, #4483, .T. ) ;
#6059=CARTESIAN_POINT ( 'NONE',  ( 0.000000000000000000, 0.000000000000000000, -175.0000000000000284 ) ) ;
#6069=VECTOR ( 'NONE', #4584, 1000.000000000000000 ) ;
#6072=EDGE_LOOP ( 'NONE', ( #4246, #3795, #3305, #3698 ) ) ;
#6075=VECTOR ( 'NONE', #4022, 1000.000000000000000 ) ;
#6077=FACE_BOUND ( 'NONE', #3684, .T. ) ;
#6078=CARTESIAN_POINT ( 'NONE',  ( 13.14183123006966980, -39.58265509608656174, -115.0000000000000000 ) ) ;
#6091=PLANE ( 'NONE',  #731 ) ;
#6094=EDGE_CURVE ( 'NONE', #6280, #4938, #6149, .T. ) ;
#6099=VERTEX_POINT ( 'NONE', #292 ) ;
#6102=CARTESIAN_POINT ( 'NONE',  ( -43.99999999999987921, 13.41640786499904969, -115.0000000000000000 ) ) ;
#6103=AXIS2_PLACEMENT_3D ( 'NONE', #5128, #6229, #6125 ) ;
#6104=DIRECTION ( 'NONE',  ( -0.000000000000000000, -0.000000000000000000, 1.000000000000000000 ) ) ;
#6105=EDGE_CURVE ( 'NONE', #3220, #1488, #6345, .T. ) ;
#6108=DIRECTION ( 'NONE',  ( -0.000000000000000000, 0.000000000000000000, -1.000000000000000000 ) ) ;
#6110=CARTESIAN_POINT ( 'NONE',  ( 0.000000000000000000, 0.000000000000000000, -175.0000000000000000 ) ) ;
#6112=ORIENTED_EDGE ( 'NONE', *, *, #3690, .F. ) ;
#6113=PRODUCT_DEFINITION_SHAPE ( 'NONE', 'NONE',  #1725 ) ;
#6115=VERTEX_POINT ( 'NONE', #3339 ) ;
#6118=( NAMED_UNIT ( * ) SI_UNIT ( $, .STERADIAN. ) SOLID_ANGLE_UNIT ( ) );
#6122=ORIENTED_EDGE ( 'NONE', *, *, #3334, .F. ) ;
#6125=DIRECTION ( 'NONE',  ( -1.000000000000000000, 0.000000000000000000, 0.000000000000000000 ) ) ;
#6131=DIRECTION ( 'NONE',  ( -0.000000000000000000, -0.000000000000000000, -1.000000000000000000 ) ) ;
#6134=PLANE ( 'NONE',  #3589 ) ;
#6142=CARTESIAN_POINT ( 'NONE',  ( 0.2052511266213280505, 21.25619793154159964, 0.000000000000000000 ) ) ;
#6145=DIRECTION ( 'NONE',  ( -1.000000000000000000, 0.000000000000000000, 0.000000000000000000 ) ) ;
#6147=DIRECTION ( 'NONE',  ( -0.000000000000000000, 0.000000000000000000, -1.000000000000000000 ) ) ;
#6148=ADVANCED_FACE ( 'NONE', ( #2281 ), #3247, .T. ) ;
#6149=LINE ( 'NONE', #1378, #5019 ) ;
#6151=CARTESIAN_POINT ( 'NONE',  ( 0.000000000000000000, 0.000000000000000000, -248.0000000000000000 ) ) ;
#6156=FACE_OUTER_BOUND ( 'NONE', #3319, .T. ) ;
#6157=CIRCLE ( 'NONE', #1532, 17.00000000000000000 ) ;
#6160=VERTEX_POINT ( 'NONE', #2797 ) ;
#6162=EDGE_CURVE ( 'NONE', #6160, #4541, #3703, .T. ) ;
#6164=FACE_OUTER_BOUND ( 'NONE', #4301, .T. ) ;
#6169=DIRECTION ( 'NONE',  ( -0.000000000000000000, -0.000000000000000000, 1.000000000000000000 ) ) ;
#6171=ADVANCED_FACE ( 'NONE', ( #4242 ), #2722, .T. ) ;
#6175=CARTESIAN_POINT ( 'NONE',  ( 16.23652742703164975, 37.28747423195200383, -180.0000000000000000 ) ) ;
#6178=FACE_OUTER_BOUND ( 'NONE', #3752, .T. ) ;
#6180=ADVANCED_FACE ( 'NONE', ( #4769, #1872 ), #6222, .F. ) ;
#6184=ORIENTED_EDGE ( 'NONE', *, *, #3045, .T. ) ;
#6185=DIRECTION ( 'NONE',  ( -1.000000000000000000, 0.000000000000000000, 0.000000000000000000 ) ) ;
#6186=AXIS2_PLACEMENT_3D ( 'NONE', #3041, #2557, #4489 ) ;
#6187=DIRECTION ( 'NONE',  ( 1.000000000000000000, 0.000000000000000000, 0.000000000000000000 ) ) ;
#6193=ORIENTED_EDGE ( 'NONE', *, *, #752, .T. ) ;
#6196=AXIS2_PLACEMENT_3D ( 'NONE', #681, #2119, #1524 ) ;
#6197=CARTESIAN_POINT ( 'NONE',  ( -13.14183123006980480, 39.58265509608657595, -195.0000000000000000 ) ) ;
#6201=CYLINDRICAL_SURFACE ( 'NONE', #2087, 89.87058297576894006 ) ;
#6205=DIRECTION ( 'NONE',  ( 1.000000000000000000, 0.000000000000000000, 0.000000000000000000 ) ) ;
#6208=CIRCLE ( 'NONE', #2502, 17.00000000000000000 ) ;
#6209=EDGE_CURVE ( 'NONE', #1569, #2747, #1607, .T. ) ;
#6215=DIRECTION ( 'NONE',  ( -0.000000000000000000, -0.000000000000000000, 1.000000000000000000 ) ) ;
#6217=EDGE_CURVE ( 'NONE', #5105, #4956, #4908, .T. ) ;
#6222=PLANE ( 'NONE',  #4488 ) ;
#6225=ORIENTED_EDGE ( 'NONE', *, *, #2721, .F. ) ;
#6229=DIRECTION ( 'NONE',  ( 0.000000000000000000, 0.000000000000000000, -1.000000000000000000 ) ) ;
#6234=ORIENTED_EDGE ( 'NONE', *, *, #2000, .F. ) ;
#6235=DIRECTION ( 'NONE',  ( -0.000000000000000000, 0.000000000000000000, -1.000000000000000000 ) ) ;
#6240=ORIENTED_EDGE ( 'NONE', *, *, #2483, .T. ) ;
#6244=AXIS2_PLACEMENT_3D ( 'NONE', #3244, #841, #5216 ) ;
#6248=CARTESIAN_POINT ( 'NONE',  ( 17.00000000000000000, 0.000000000000000000, -49.99999999999999289 ) ) ;
#6251=DIRECTION ( 'NONE',  ( 1.000000000000000000, 0.000000000000000000, 0.000000000000000000 ) ) ;
#6252=CARTESIAN_POINT ( 'NONE',  ( -17.00000000000000000, 0.000000000000000000, 48.00000000000000000 ) ) ;
#6253=FACE_OUTER_BOUND ( 'NONE', #2208, .T. ) ;
#6254=EDGE_LOOP ( 'NONE', ( #5811, #5200, #1598, #1328 ) ) ;
#6258=LINE ( 'NONE', #4280, #1778 ) ;
#6269=CARTESIAN_POINT ( 'NONE',  ( -44.43364355155666345, 29.42304313293565343, -175.0000000000000284 ) ) ;
#6270=ORIENTED_EDGE ( 'NONE', *, *, #2310, .F. ) ;
#6271=ORIENTED_EDGE ( 'NONE', *, *, #4353, .T. ) ;
#6274=AXIS2_PLACEMENT_3D ( 'NONE', #124, #572, #5925 ) ;
#6278=CIRCLE ( 'NONE', #3496, 22.67164836619066648 ) ;
#6280=VERTEX_POINT ( 'NONE', #1899 ) ;
#6282=DIRECTION ( 'NONE',  ( -1.000000000000000000, 0.000000000000000000, 0.000000000000000000 ) ) ;
#6287=EDGE_LOOP ( 'NONE', ( #755, #3950, #1286, #2979 ) ) ;
#6289=AXIS2_PLACEMENT_3D ( 'NONE', #1862, #2816, #1343 ) ;
#6290=CARTESIAN_POINT ( 'NONE',  ( -22.21770253897380343, -3.871672004622680241, -195.0000000000000000 ) ) ;
#6292=EDGE_CURVE ( 'NONE', #673, #3260, #2335, .T. ) ;
#6296=CARTESIAN_POINT ( 'NONE',  ( -16.23652742703189489, -37.28747423195188304, -115.0000000000000000 ) ) ;
#6300=AXIS2_PLACEMENT_3D ( 'NONE', #4170, #1871, #777 ) ;
#6310=CARTESIAN_POINT ( 'NONE',  ( -43.99999999999987921, 13.41640786499904969, -130.0000000000000000 ) ) ;
#6311=ADVANCED_FACE ( 'NONE', ( #1000 ), #4925, .T. ) ;
#6318=CARTESIAN_POINT ( 'NONE',  ( 17.00000000000000000, 0.000000000000000000, -115.0000000000000000 ) ) ;
#6322=DIRECTION ( 'NONE',  ( -0.000000000000000000, -0.000000000000000000, 1.000000000000000000 ) ) ;
#6327=CYLINDRICAL_SURFACE ( 'NONE', #4131, 17.00000000000000000 ) ;
#6328=CARTESIAN_POINT ( 'NONE',  ( -17.00000000000000355, -24.99999999999999645, -95.00000000000000000 ) ) ;
#6330=DIRECTION ( 'NONE',  ( 1.000000000000000000, 0.000000000000000000, -0.000000000000000000 ) ) ;
#6338=LINE ( 'NONE', #1445, #1188 ) ;
#6342=ORIENTED_EDGE ( 'NONE', *, *, #5069, .T. ) ;
#6345=CIRCLE ( 'NONE', #4293, 46.00000000000000000 ) ;
#6346=DIRECTION ( 'NONE',  ( -0.000000000000000000, -0.000000000000000000, 1.000000000000000000 ) ) ;
#6348=DIRECTION ( 'NONE',  ( -0.000000000000000000, -0.000000000000000000, 1.000000000000000000 ) ) ;
#6349=AXIS2_PLACEMENT_3D ( 'NONE', #290, #2242, #4169 ) ;
#6351=ORIENTED_EDGE ( 'NONE', *, *, #2867, .F. ) ;
#6352=DIRECTION ( 'NONE',  ( -0.000000000000000000, 0.000000000000000000, -1.000000000000000000 ) ) ;
#6354=DIRECTION ( 'NONE',  ( -0.000000000000000000, -0.000000000000000000, -1.000000000000000000 ) ) ;
#6359=CARTESIAN_POINT ( 'NONE',  ( -44.64065620456596406, -28.99954194078535963, 15.00000000000000000 ) ) ;
#6360=ORIENTED_EDGE ( 'NONE', *, *, #4181, .T. ) ;
#6361=AXIS2_PLACEMENT_3D ( 'NONE', #2684, #3233, #951 ) ;
#6362=CIRCLE ( 'NONE', #4825, 46.00000000000000000 ) ;
#6392=COLOUR_RGB('Sky Blue',0.24,0.69,0.87);
#6393=FILL_AREA_STYLE_COLOUR('',#6392);
#6394=FILL_AREA_STYLE('',(#6393));
#6395=SURFACE_STYLE_FILL_AREA(#6394);
#6396=SURFACE_SIDE_STYLE('',(#6395));
#6397=SURFACE_STYLE_USAGE(.BOTH.,#6396);
#6398=PRESENTATION_STYLE_ASSIGNMENT((#6397));
ENDSEC;
END-ISO-10303-21;
